ISO-10303-21;
HEADER;
/* Generated by software containing ST-Developer
 * from STEP Tools, Inc. (www.steptools.com) 
 */
/* OPTION: using custom renumber hook */

FILE_DESCRIPTION(
/* description */ ('STEP AP242 Edition 2', 'CAx-IF Rec.Pracs.---Representation and Presentation of Product Manufa
cturing Information (PMI)---4.0---2014-10-13', 'CAx-IF Rec.Pracs.---3D Tessellated Geometry---0.4---2014-09-14', '2;1', 'CAx-IF Rec.Pracs.---User Defined Attributes---1.5---2016-08-15'),
/* implementation_level */ '2;1');

FILE_NAME(
/* name */ 'refill_screw.step',
/* time_stamp */ '2026-10-08T12:15:07Z',
/* author */ (''),
/* organization */ (''),
/* preprocessor_version */ 'ST-DEVELOPER v20',
/* originating_system */ 'ONSHAPE BY PTC INC, 1.221',
/* authorisation */ '  ');

FILE_SCHEMA (('AP242_MANAGED_MODEL_BASED_3D_ENGINEERING_MIM_LF { 1 0 10303 442 3 1 4 }'));
ENDSEC;

DATA;
#55=B_SPLINE_SURFACE_WITH_KNOTS('',3,3,((#40363,#40364,#40365,#40366,#40367,
#40368,#40369,#40370,#40371,#40372,#40373,#40374,#40375,#40376,#40377,#40378,
#40379,#40380,#40381,#40382,#40383,#40384,#40385,#40386,#40387,#40388,#40389,
#40390,#40391,#40392,#40393,#40394,#40395,#40396,#40397,#40398,#40399,#40400,
#40401,#40402,#40403,#40404,#40405,#40406,#40407,#40408,#40409,#40410,#40411,
#40412,#40413,#40414,#40415,#40416,#40417,#40418,#40419,#40420,#40421,#40422,
#40423,#40424,#40425,#40426,#40427,#40428,#40429,#40430,#40431,#40432,#40433,
#40434,#40435,#40436,#40437,#40438,#40439,#40440,#40441,#40442,#40443,#40444,
#40445,#40446,#40447,#40448,#40449,#40450,#40451,#40452,#40453,#40454,#40455,
#40456,#40457,#40458,#40459,#40460,#40461,#40462,#40463,#40464,#40465,#40466,
#40467,#40468,#40469,#40470,#40471,#40472,#40473,#40474,#40475,#40476),
(#40477,#40478,#40479,#40480,#40481,#40482,#40483,#40484,#40485,#40486,
#40487,#40488,#40489,#40490,#40491,#40492,#40493,#40494,#40495,#40496,#40497,
#40498,#40499,#40500,#40501,#40502,#40503,#40504,#40505,#40506,#40507,#40508,
#40509,#40510,#40511,#40512,#40513,#40514,#40515,#40516,#40517,#40518,#40519,
#40520,#40521,#40522,#40523,#40524,#40525,#40526,#40527,#40528,#40529,#40530,
#40531,#40532,#40533,#40534,#40535,#40536,#40537,#40538,#40539,#40540,#40541,
#40542,#40543,#40544,#40545,#40546,#40547,#40548,#40549,#40550,#40551,#40552,
#40553,#40554,#40555,#40556,#40557,#40558,#40559,#40560,#40561,#40562,#40563,
#40564,#40565,#40566,#40567,#40568,#40569,#40570,#40571,#40572,#40573,#40574,
#40575,#40576,#40577,#40578,#40579,#40580,#40581,#40582,#40583,#40584,#40585,
#40586,#40587,#40588,#40589,#40590),(#40591,#40592,#40593,#40594,#40595,
#40596,#40597,#40598,#40599,#40600,#40601,#40602,#40603,#40604,#40605,#40606,
#40607,#40608,#40609,#40610,#40611,#40612,#40613,#40614,#40615,#40616,#40617,
#40618,#40619,#40620,#40621,#40622,#40623,#40624,#40625,#40626,#40627,#40628,
#40629,#40630,#40631,#40632,#40633,#40634,#40635,#40636,#40637,#40638,#40639,
#40640,#40641,#40642,#40643,#40644,#40645,#40646,#40647,#40648,#40649,#40650,
#40651,#40652,#40653,#40654,#40655,#40656,#40657,#40658,#40659,#40660,#40661,
#40662,#40663,#40664,#40665,#40666,#40667,#40668,#40669,#40670,#40671,#40672,
#40673,#40674,#40675,#40676,#40677,#40678,#40679,#40680,#40681,#40682,#40683,
#40684,#40685,#40686,#40687,#40688,#40689,#40690,#40691,#40692,#40693,#40694,
#40695,#40696,#40697,#40698,#40699,#40700,#40701,#40702,#40703,#40704),
(#40705,#40706,#40707,#40708,#40709,#40710,#40711,#40712,#40713,#40714,
#40715,#40716,#40717,#40718,#40719,#40720,#40721,#40722,#40723,#40724,#40725,
#40726,#40727,#40728,#40729,#40730,#40731,#40732,#40733,#40734,#40735,#40736,
#40737,#40738,#40739,#40740,#40741,#40742,#40743,#40744,#40745,#40746,#40747,
#40748,#40749,#40750,#40751,#40752,#40753,#40754,#40755,#40756,#40757,#40758,
#40759,#40760,#40761,#40762,#40763,#40764,#40765,#40766,#40767,#40768,#40769,
#40770,#40771,#40772,#40773,#40774,#40775,#40776,#40777,#40778,#40779,#40780,
#40781,#40782,#40783,#40784,#40785,#40786,#40787,#40788,#40789,#40790,#40791,
#40792,#40793,#40794,#40795,#40796,#40797,#40798,#40799,#40800,#40801,#40802,
#40803,#40804,#40805,#40806,#40807,#40808,#40809,#40810,#40811,#40812,#40813,
#40814,#40815,#40816,#40817,#40818)),.UNSPECIFIED.,.F.,.F.,.F.,(4,4),(4,
2,2,2,2,2,2,2,2,2,2,2,2,2,2,2,2,2,2,2,2,2,2,2,2,2,2,2,2,2,2,2,2,2,2,2,2,
2,2,2,2,2,2,2,2,2,2,2,2,2,2,2,2,2,2,2,4),(0.,1.),(0.,0.0151615249539755,
0.0303230499079509,0.0454845748619264,0.0606460998159018,0.0909691497238527,
0.106130674677828,0.121292199631804,0.136453724585779,0.151615249539755,
0.16677677449373,0.181938299447705,0.197099824401681,0.212261349355656,
0.242584399263607,0.257745924217583,0.272907449171558,0.303230499079509,
0.318392024033485,0.33355354898746,0.363876598895411,0.379038123849386,
0.394199648803362,0.409361173757337,0.424522698711313,0.439684223665288,
0.454845748619264,0.470007273573239,0.485168798527215,0.515491848435166,
0.530653373389141,0.545814898343116,0.560976423297092,0.576137948251067,
0.591299473205043,0.606460998159018,0.621622523112994,0.636784048066969,
0.66710709797492,0.682268622928896,0.697430147882871,0.727753197790822,
0.742914722744797,0.758076247698773,0.788399297606724,0.803560822560699,
0.818722347514675,0.83388387246865,0.849045397422626,0.864206922376601,
0.879368447330577,0.894529972284552,0.909691497238527,0.940014547146478,
0.955176072100454,0.962756834577442,0.970337597054429),.UNSPECIFIED.);
#60=COLOUR_RGB('', 0.66274510, 0.83137255, 0.94901961);
#223=SHAPE_REPRESENTATION_RELATIONSHIP('','',#13797,#250);
#250=ADVANCED_BREP_SHAPE_REPRESENTATION('',(#13741),#45487);
#950=CIRCLE('',#15085,0.00736858102143575);
#951=CIRCLE('',#15086,0.00736858102143575);
#952=CIRCLE('',#15087,0.00736858102143575);
#953=CIRCLE('',#15088,0.00736858102143575);
#954=CIRCLE('',#15089,0.00736858102143575);
#955=CIRCLE('',#15090,0.00736858102143575);
#956=CIRCLE('',#15091,0.00736858102143575);
#957=CIRCLE('',#15092,0.00736858102143575);
#958=CIRCLE('',#15093,0.00736858102143575);
#959=CIRCLE('',#15094,0.00736858102143575);
#960=CIRCLE('',#15095,0.00736858102143575);
#961=CIRCLE('',#15096,0.0004);
#962=CIRCLE('',#15098,0.00736858102143575);
#963=CIRCLE('',#15099,0.00736858102143575);
#964=CIRCLE('',#15100,0.00736858102143575);
#965=CIRCLE('',#15101,0.00736858102143575);
#966=CIRCLE('',#15102,0.00736858102143575);
#967=CIRCLE('',#15103,0.00736858102143575);
#968=CIRCLE('',#15104,0.00736858102143575);
#969=CIRCLE('',#15105,0.00736858102143575);
#970=CIRCLE('',#15106,0.00736858102143575);
#971=CIRCLE('',#15107,0.00736858102143575);
#972=CIRCLE('',#15108,0.00736858102143575);
#973=CIRCLE('',#15109,0.005);
#974=CIRCLE('',#15112,0.005);
#975=CIRCLE('',#15113,0.0004);
#1147=B_SPLINE_CURVE_WITH_KNOTS('',3,(#40277,#40278,#40279,#40280),
 .UNSPECIFIED.,.F.,.F.,(4,4),(6.48381396703939E-18,0.00339130657297538),
 .UNSPECIFIED.);
#1475=PLANE('',#15049);
#1476=PLANE('',#15050);
#1477=PLANE('',#15051);
#1478=PLANE('',#15052);
#1479=PLANE('',#15053);
#1480=PLANE('',#15054);
#1481=PLANE('',#15055);
#1482=PLANE('',#15056);
#1483=PLANE('',#15057);
#1484=PLANE('',#15058);
#1485=PLANE('',#15059);
#1486=PLANE('',#15060);
#1487=PLANE('',#15061);
#1488=PLANE('',#15062);
#1489=PLANE('',#15063);
#1490=PLANE('',#15064);
#1491=PLANE('',#15065);
#1492=PLANE('',#15066);
#1493=PLANE('',#15067);
#1494=PLANE('',#15068);
#1495=PLANE('',#15069);
#1496=PLANE('',#15070);
#1497=PLANE('',#15071);
#1498=PLANE('',#15072);
#1499=PLANE('',#15073);
#1500=PLANE('',#15074);
#1501=PLANE('',#15075);
#1502=PLANE('',#15076);
#1503=PLANE('',#15077);
#1504=PLANE('',#15078);
#1505=PLANE('',#15079);
#1506=PLANE('',#15080);
#1507=PLANE('',#15081);
#1508=PLANE('',#15082);
#1509=PLANE('',#15083);
#1510=PLANE('',#15084);
#1511=PLANE('',#15097);
#1512=PLANE('',#15111);
#1779=CYLINDRICAL_SURFACE('',#15110,0.00736858102143575);
#1780=CYLINDRICAL_SURFACE('',#15114,0.00736858102143575);
#1781=CYLINDRICAL_SURFACE('',#15115,0.00736858102143575);
#1782=CYLINDRICAL_SURFACE('',#15116,0.00736858102143575);
#1783=CYLINDRICAL_SURFACE('',#15117,0.00736858102143575);
#1784=CYLINDRICAL_SURFACE('',#15118,0.00736858102143575);
#1785=CYLINDRICAL_SURFACE('',#15119,0.00736858102143575);
#1786=CYLINDRICAL_SURFACE('',#15120,0.00736858102143575);
#1787=CYLINDRICAL_SURFACE('',#15121,0.00736858102143575);
#1788=CYLINDRICAL_SURFACE('',#15122,0.00736858102143575);
#1789=CYLINDRICAL_SURFACE('',#15123,0.00736858102143575);
#1790=CYLINDRICAL_SURFACE('',#15124,0.005);
#1791=CYLINDRICAL_SURFACE('',#15125,0.0004);
#1929=(
BOUNDED_CURVE()
B_SPLINE_CURVE(2,(#39732,#39733,#39734,#39735,#39736,#39737,#39738,#39739,
#39740,#39741,#39742,#39743,#39744,#39745,#39746,#39747,#39748,#39749,#39750,
#39751,#39752,#39753,#39754,#39755,#39756,#39757,#39758,#39759,#39760,#39761,
#39762,#39763,#39764,#39765,#39766,#39767,#39768,#39769,#39770,#39771,#39772,
#39773,#39774,#39775,#39776,#39777,#39778,#39779,#39780,#39781,#39782,#39783,
#39784,#39785,#39786,#39787,#39788,#39789,#39790,#39791,#39792,#39793,#39794,
#39795,#39796,#39797,#39798,#39799,#39800,#39801,#39802,#39803,#39804,#39805,
#39806,#39807,#39808,#39809,#39810),.UNSPECIFIED.,.F.,.F.)
B_SPLINE_CURVE_WITH_KNOTS((3,2,2,2,2,2,2,2,2,2,2,2,2,2,2,2,2,2,2,2,2,2,
2,2,2,2,2,2,2,2,2,2,2,2,2,2,2,2,2,3),(0.,0.025,0.05,0.075,0.1,0.125,0.15,
0.175,0.2,0.225,0.25,0.275,0.3,0.325,0.35,0.375,0.4,0.425,0.45,0.475,0.5,
0.525,0.55,0.575,0.6,0.625,0.65,0.675,0.7,0.725,0.75,0.775,0.8,0.825,0.85,
0.875,0.9,0.925,0.95,0.964550284056263),.UNSPECIFIED.)
CURVE()
GEOMETRIC_REPRESENTATION_ITEM()
RATIONAL_B_SPLINE_CURVE((1.,0.951056516295154,1.,0.951056516295154,1.,0.951056516295154,
1.,0.951056516295154,1.,0.951056516295154,1.,0.951056516295154,1.,0.951056516295154,
1.,0.951056516295154,1.,0.951056516295154,1.,0.951056516295154,1.,0.951056516295154,
1.,0.951056516295154,1.,0.951056516295154,1.,0.951056516295154,1.,0.951056516295154,
1.,0.951056516295154,1.,0.951056516295154,1.,0.951056516295154,1.,0.951056516295154,
1.,0.951056516295154,1.,0.951056516295154,1.,0.951056516295154,1.,0.951056516295154,
1.,0.951056516295154,1.,0.951056516295154,1.,0.951056516295154,1.,0.951056516295154,
1.,0.951056516295154,1.,0.951056516295154,1.,0.951056516295154,1.,0.951056516295154,
1.,0.951056516295154,1.,0.951056516295154,1.,0.951056516295154,1.,0.951056516295154,
1.,0.951056516295154,1.,0.951056516295154,1.,0.951056516295154,1.,0.971514336375656,
0.976186632532541))
REPRESENTATION_ITEM('')
);
#1930=(
BOUNDED_CURVE()
B_SPLINE_CURVE(2,(#39814,#39815,#39816,#39817,#39818),.UNSPECIFIED.,.F.,
 .F.)
B_SPLINE_CURVE_WITH_KNOTS((3,2,3),(0.9375,0.95,0.9645502840563),
 .UNSPECIFIED.)
CURVE()
GEOMETRIC_REPRESENTATION_ITEM()
RATIONAL_B_SPLINE_CURVE((0.975528258147577,0.975528258147577,1.,0.971514336375583,
0.976186632532565))
REPRESENTATION_ITEM('')
);
#1931=(
BOUNDED_CURVE()
B_SPLINE_CURVE(2,(#39820,#39821,#39822,#39823,#39824,#39825,#39826,#39827,
#39828,#39829,#39830,#39831,#39832),.UNSPECIFIED.,.F.,.F.)
B_SPLINE_CURVE_WITH_KNOTS((3,2,2,2,2,2,3),(0.8125,0.825,0.85,0.875,0.9,
0.925,0.9375),.UNSPECIFIED.)
CURVE()
GEOMETRIC_REPRESENTATION_ITEM()
RATIONAL_B_SPLINE_CURVE((0.975528258147577,0.975528258147577,1.,0.951056516295154,
1.,0.951056516295154,1.,0.951056516295154,1.,0.951056516295154,1.,0.975528258147577,
0.975528258147577))
REPRESENTATION_ITEM('')
);
#1932=(
BOUNDED_CURVE()
B_SPLINE_CURVE(2,(#39834,#39835,#39836,#39837,#39838,#39839,#39840,#39841,
#39842,#39843,#39844,#39845,#39846),.UNSPECIFIED.,.F.,.F.)
B_SPLINE_CURVE_WITH_KNOTS((3,2,2,2,2,2,3),(0.6875,0.7,0.725,0.75,0.775,
0.8,0.8125),.UNSPECIFIED.)
CURVE()
GEOMETRIC_REPRESENTATION_ITEM()
RATIONAL_B_SPLINE_CURVE((0.975528258147577,0.975528258147577,1.,0.951056516295154,
1.,0.951056516295154,1.,0.951056516295154,1.,0.951056516295154,1.,0.975528258147577,
0.975528258147577))
REPRESENTATION_ITEM('')
);
#1933=(
BOUNDED_CURVE()
B_SPLINE_CURVE(2,(#39848,#39849,#39850,#39851,#39852,#39853,#39854,#39855,
#39856,#39857,#39858,#39859,#39860),.UNSPECIFIED.,.F.,.F.)
B_SPLINE_CURVE_WITH_KNOTS((3,2,2,2,2,2,3),(0.5625,0.575,0.6,0.625,0.65,
0.675,0.6875),.UNSPECIFIED.)
CURVE()
GEOMETRIC_REPRESENTATION_ITEM()
RATIONAL_B_SPLINE_CURVE((0.975528258147577,0.975528258147577,1.,0.951056516295154,
1.,0.951056516295154,1.,0.951056516295154,1.,0.951056516295154,1.,0.975528258147577,
0.975528258147577))
REPRESENTATION_ITEM('')
);
#1934=(
BOUNDED_CURVE()
B_SPLINE_CURVE(2,(#39862,#39863,#39864,#39865,#39866,#39867,#39868,#39869,
#39870,#39871,#39872,#39873,#39874),.UNSPECIFIED.,.F.,.F.)
B_SPLINE_CURVE_WITH_KNOTS((3,2,2,2,2,2,3),(0.4375,0.45,0.475,0.5,0.525,
0.55,0.5625),.UNSPECIFIED.)
CURVE()
GEOMETRIC_REPRESENTATION_ITEM()
RATIONAL_B_SPLINE_CURVE((0.975528258147577,0.975528258147577,1.,0.951056516295154,
1.,0.951056516295154,1.,0.951056516295154,1.,0.951056516295154,1.,0.975528258147577,
0.975528258147577))
REPRESENTATION_ITEM('')
);
#1935=(
BOUNDED_CURVE()
B_SPLINE_CURVE(2,(#39876,#39877,#39878,#39879,#39880,#39881,#39882,#39883,
#39884,#39885,#39886,#39887,#39888),.UNSPECIFIED.,.F.,.F.)
B_SPLINE_CURVE_WITH_KNOTS((3,2,2,2,2,2,3),(0.3125,0.325,0.35,0.375,0.4,
0.425,0.4375),.UNSPECIFIED.)
CURVE()
GEOMETRIC_REPRESENTATION_ITEM()
RATIONAL_B_SPLINE_CURVE((0.975528258147577,0.975528258147577,1.,0.951056516295154,
1.,0.951056516295154,1.,0.951056516295154,1.,0.951056516295154,1.,0.975528258147577,
0.975528258147577))
REPRESENTATION_ITEM('')
);
#1936=(
BOUNDED_CURVE()
B_SPLINE_CURVE(2,(#39890,#39891,#39892,#39893,#39894,#39895,#39896,#39897,
#39898,#39899,#39900,#39901,#39902),.UNSPECIFIED.,.F.,.F.)
B_SPLINE_CURVE_WITH_KNOTS((3,2,2,2,2,2,3),(0.1875,0.2,0.225,0.25,0.275,
0.3,0.3125),.UNSPECIFIED.)
CURVE()
GEOMETRIC_REPRESENTATION_ITEM()
RATIONAL_B_SPLINE_CURVE((0.975528258147577,0.975528258147577,1.,0.951056516295154,
1.,0.951056516295154,1.,0.951056516295154,1.,0.951056516295154,1.,0.975528258147577,
0.975528258147577))
REPRESENTATION_ITEM('')
);
#1937=(
BOUNDED_CURVE()
B_SPLINE_CURVE(2,(#39904,#39905,#39906,#39907,#39908,#39909,#39910,#39911,
#39912,#39913,#39914,#39915,#39916),.UNSPECIFIED.,.F.,.F.)
B_SPLINE_CURVE_WITH_KNOTS((3,2,2,2,2,2,3),(0.0625,0.075,0.1,0.125,0.15,
0.175,0.1875),.UNSPECIFIED.)
CURVE()
GEOMETRIC_REPRESENTATION_ITEM()
RATIONAL_B_SPLINE_CURVE((0.975528258147577,0.975528258147577,1.,0.951056516295154,
1.,0.951056516295154,1.,0.951056516295154,1.,0.951056516295154,1.,0.975528258147577,
0.975528258147577))
REPRESENTATION_ITEM('')
);
#1938=(
BOUNDED_CURVE()
B_SPLINE_CURVE(2,(#39918,#39919,#39920,#39921,#39922,#39923,#39924),
 .UNSPECIFIED.,.F.,.F.)
B_SPLINE_CURVE_WITH_KNOTS((3,2,2,3),(0.,0.025,0.05,0.0625),
 .UNSPECIFIED.)
CURVE()
GEOMETRIC_REPRESENTATION_ITEM()
RATIONAL_B_SPLINE_CURVE((1.,0.951056516295154,1.,0.951056516295154,1.,0.975528258147577,
0.975528258147577))
REPRESENTATION_ITEM('')
);
#1939=(
BOUNDED_CURVE()
B_SPLINE_CURVE(2,(#40171,#40172,#40173,#40174,#40175,#40176,#40177),
 .UNSPECIFIED.,.F.,.F.)
B_SPLINE_CURVE_WITH_KNOTS((3,2,2,3),(0.,0.00313236994712061,0.00626473989424123,
0.00783092486780153),.UNSPECIFIED.)
CURVE()
GEOMETRIC_REPRESENTATION_ITEM()
RATIONAL_B_SPLINE_CURVE((1.,0.951056516295154,1.,0.951056516295154,1.,0.975528258147577,
0.975528258147577))
REPRESENTATION_ITEM('')
);
#1940=(
BOUNDED_CURVE()
B_SPLINE_CURVE(2,(#40179,#40180,#40181,#40182,#40183,#40184,#40185,#40186,
#40187,#40188,#40189,#40190,#40191),.UNSPECIFIED.,.F.,.F.)
B_SPLINE_CURVE_WITH_KNOTS((3,2,2,2,2,2,3),(0.00783092486780153,0.00939686100434394,
0.0125287332774288,0.0156606055505136,0.0187924778235984,0.0219243500966832,
0.0234902862332256),.UNSPECIFIED.)
CURVE()
GEOMETRIC_REPRESENTATION_ITEM()
RATIONAL_B_SPLINE_CURVE((0.975528258147577,0.975528258147577,1.,0.951056516295154,
1.,0.951056516295154,1.,0.951056516295154,1.,0.951056516295154,1.,0.975528258147577,
0.975528258147577))
REPRESENTATION_ITEM('')
);
#1941=(
BOUNDED_CURVE()
B_SPLINE_CURVE(2,(#40193,#40194,#40195,#40196,#40197,#40198,#40199,#40200,
#40201,#40202,#40203,#40204,#40205),.UNSPECIFIED.,.F.,.F.)
B_SPLINE_CURVE_WITH_KNOTS((3,2,2,2,2,2,3),(0.0234902862332256,0.0250560316219713,
0.0281875223994624,0.0313190131769537,0.0344505039544449,0.0375819947319362,
0.0391477401206671),.UNSPECIFIED.)
CURVE()
GEOMETRIC_REPRESENTATION_ITEM()
RATIONAL_B_SPLINE_CURVE((0.975528258147577,0.975528258147577,1.,0.951056516295154,
1.,0.951056516295154,1.,0.951056516295154,1.,0.951056516295154,1.,0.975528258147807,
0.975528258147577))
REPRESENTATION_ITEM('')
);
#1942=(
BOUNDED_CURVE()
B_SPLINE_CURVE(2,(#40207,#40208,#40209,#40210,#40211,#40212,#40213,#40214,
#40215,#40216,#40217,#40218,#40219),.UNSPECIFIED.,.F.,.F.)
B_SPLINE_CURVE_WITH_KNOTS((3,2,2,2,2,2,3),(0.0391477401206671,0.0407138913050886,
0.0438461936739023,0.0469784960427159,0.0501107984115296,0.0532431007803432,
0.0548092519647501),.UNSPECIFIED.)
CURVE()
GEOMETRIC_REPRESENTATION_ITEM()
RATIONAL_B_SPLINE_CURVE((0.975528258147577,0.975528258147347,1.,0.951056516295154,
1.,0.951056516295154,1.,0.951056516295154,1.,0.951056516295154,1.,0.975528258147577,
0.975528258147577))
REPRESENTATION_ITEM('')
);
#1943=(
BOUNDED_CURVE()
B_SPLINE_CURVE(2,(#40221,#40222,#40223,#40224,#40225,#40226,#40227,#40228,
#40229,#40230,#40231,#40232,#40233),.UNSPECIFIED.,.F.,.F.)
B_SPLINE_CURVE_WITH_KNOTS((3,2,2,2,2,2,3),(0.0548092519647501,0.0563753388810186,
0.0595075127135556,0.0626396865460927,0.0657718603786298,0.0689040342111668,
0.0704701211274353),.UNSPECIFIED.)
CURVE()
GEOMETRIC_REPRESENTATION_ITEM()
RATIONAL_B_SPLINE_CURVE((0.975528258147577,0.975528258147577,1.,0.951056516295154,
1.,0.951056516295154,1.,0.951056516295154,1.,0.951056516295154,1.,0.975528258147577,
0.975528258147577))
REPRESENTATION_ITEM('')
);
#1944=(
BOUNDED_CURVE()
B_SPLINE_CURVE(2,(#40235,#40236,#40237,#40238,#40239,#40240,#40241,#40242,
#40243,#40244,#40245,#40246,#40247),.UNSPECIFIED.,.F.,.F.)
B_SPLINE_CURVE_WITH_KNOTS((3,2,2,2,2,2,3),(0.0704701211274353,0.0720358098879434,
0.0751671874089597,0.0782985649299759,0.0814299424509921,0.0845613199720083,
0.0861270087324948),.UNSPECIFIED.)
CURVE()
GEOMETRIC_REPRESENTATION_ITEM()
RATIONAL_B_SPLINE_CURVE((0.975528258147577,0.975528258147577,1.,0.951056516295154,
1.,0.951056516295154,1.,0.951056516295154,1.,0.951056516295154,1.,0.975528258147915,
0.975528258147577))
REPRESENTATION_ITEM('')
);
#1945=(
BOUNDED_CURVE()
B_SPLINE_CURVE(2,(#40249,#40250,#40251,#40252,#40253,#40254,#40255,#40256,
#40257,#40258,#40259,#40260,#40261),.UNSPECIFIED.,.F.,.F.)
B_SPLINE_CURVE_WITH_KNOTS((3,2,2,2,2,2,3),(0.0861270087324948,0.0876930566782528,
0.0908251525697255,0.0939572484611982,0.0970893443526709,0.100221440244144,
0.10178748818988),.UNSPECIFIED.)
CURVE()
GEOMETRIC_REPRESENTATION_ITEM()
RATIONAL_B_SPLINE_CURVE((0.975528258147577,0.975528258147239,1.,0.951056516295154,
1.,0.951056516295154,1.,0.951056516295154,1.,0.951056516295154,1.,0.975528258147576,
0.975528258147577))
REPRESENTATION_ITEM('')
);
#1946=(
BOUNDED_CURVE()
B_SPLINE_CURVE(2,(#40263,#40264,#40265,#40266,#40267,#40268,#40269,#40270,
#40271,#40272,#40273,#40274,#40275),.UNSPECIFIED.,.F.,.F.)
B_SPLINE_CURVE_WITH_KNOTS((3,2,2,2,2,2,3),(0.10178748818988,0.10335365715109,
0.106485995073509,0.109618332995928,0.112750670918347,0.115883008840766,
0.117449177801976),.UNSPECIFIED.)
CURVE()
GEOMETRIC_REPRESENTATION_ITEM()
RATIONAL_B_SPLINE_CURVE((0.975528258147577,0.975528258147577,1.,0.951056516295154,
1.,0.951056516295154,1.,0.951056516295154,1.,0.951056516295154,1.,0.97552825814758,
0.975528258147577))
REPRESENTATION_ITEM('')
);
#1947=(
BOUNDED_CURVE()
B_SPLINE_CURVE(2,(#40284,#40285,#40286,#40287,#40288,#40289,#40290,#40291,
#40292,#40293,#40294,#40295,#40296,#40297,#40298,#40299,#40300,#40301,#40302,
#40303,#40304,#40305,#40306,#40307,#40308,#40309,#40310,#40311,#40312,#40313,
#40314,#40315,#40316,#40317,#40318,#40319,#40320,#40321,#40322,#40323,#40324,
#40325,#40326,#40327,#40328,#40329,#40330,#40331,#40332,#40333,#40334,#40335,
#40336,#40337,#40338,#40339,#40340,#40341,#40342,#40343,#40344,#40345,#40346,
#40347,#40348,#40349,#40350,#40351,#40352,#40353,#40354,#40355,#40356,#40357,
#40358,#40359,#40360,#40361,#40362),.UNSPECIFIED.,.F.,.F.)
B_SPLINE_CURVE_WITH_KNOTS((3,2,2,2,2,2,2,2,2,2,2,2,2,2,2,2,2,2,2,2,2,2,
2,2,2,2,2,2,2,2,2,2,2,2,2,2,2,2,2,3),(0.,0.0259188146157259,0.0518376292314517,
0.0777564438471776,0.103675258462903,0.129594073078629,0.155512887694355,
0.181431702310081,0.207350516925807,0.233269331541533,0.259188146157258,
0.285106960772985,0.311025775388711,0.336944590004436,0.362863404620162,
0.388782219235888,0.414701033851614,0.440619848467339,0.466538663083066,
0.492457477698791,0.518376292314517,0.544295106930243,0.570213921545969,
0.596132736161695,0.622051550777421,0.647970365393147,0.673889180008872,
0.699807994624598,0.725726809240324,0.75164562385605,0.777564438471776,
0.803483253087502,0.829402067703228,0.855320882318953,0.881239696934679,
0.907158511550405,0.933077326166131,0.958996140781857,0.984914955397583,
1.),.UNSPECIFIED.)
CURVE()
GEOMETRIC_REPRESENTATION_ITEM()
RATIONAL_B_SPLINE_CURVE((1.,0.951056516295154,1.,0.951056516295154,1.,0.951056516295154,
1.,0.951056516295154,1.,0.951056516295154,1.,0.951056516295154,1.,0.951056516295154,
1.,0.951056516295154,1.,0.951056516295154,1.,0.951056516295154,1.,0.951056516295154,
1.,0.951056516295154,1.,0.951056516295154,1.,0.951056516295154,1.,0.951056516295154,
1.,0.951056516295154,1.,0.951056516295154,1.,0.951056516295154,1.,0.951056516295154,
1.,0.951056516295154,1.,0.951056516295154,1.,0.951056516295154,1.,0.951056516295154,
1.,0.951056516295154,1.,0.951056516295154,1.,0.951056516295154,1.,0.951056516295154,
1.,0.951056516295154,1.,0.951056516295154,1.,0.951056516295154,1.,0.951056516295154,
1.,0.951056516295154,1.,0.951056516295154,1.,0.951056516295154,1.,0.951056516295154,
1.,0.951056516295154,1.,0.951056516295154,1.,0.951056516295154,1.,0.971514336375656,
0.976186632532541))
REPRESENTATION_ITEM('')
);
#4852=ORIENTED_EDGE('',*,*,#7073,.F.);
#4853=ORIENTED_EDGE('',*,*,#7074,.T.);
#4854=ORIENTED_EDGE('',*,*,#7075,.F.);
#4855=ORIENTED_EDGE('',*,*,#7076,.F.);
#4856=ORIENTED_EDGE('',*,*,#7077,.F.);
#4857=ORIENTED_EDGE('',*,*,#7078,.F.);
#4858=ORIENTED_EDGE('',*,*,#7079,.F.);
#4859=ORIENTED_EDGE('',*,*,#7080,.F.);
#4860=ORIENTED_EDGE('',*,*,#7081,.F.);
#4861=ORIENTED_EDGE('',*,*,#7082,.F.);
#4862=ORIENTED_EDGE('',*,*,#7083,.F.);
#4863=ORIENTED_EDGE('',*,*,#7084,.F.);
#4864=ORIENTED_EDGE('',*,*,#7085,.F.);
#4865=ORIENTED_EDGE('',*,*,#7086,.T.);
#4866=ORIENTED_EDGE('',*,*,#7087,.T.);
#4867=ORIENTED_EDGE('',*,*,#7088,.T.);
#4868=ORIENTED_EDGE('',*,*,#7089,.T.);
#4869=ORIENTED_EDGE('',*,*,#7090,.T.);
#4870=ORIENTED_EDGE('',*,*,#7091,.T.);
#4871=ORIENTED_EDGE('',*,*,#7092,.T.);
#4872=ORIENTED_EDGE('',*,*,#7093,.T.);
#4873=ORIENTED_EDGE('',*,*,#7094,.T.);
#4874=ORIENTED_EDGE('',*,*,#7095,.F.);
#4875=ORIENTED_EDGE('',*,*,#7096,.F.);
#4876=ORIENTED_EDGE('',*,*,#7097,.F.);
#4877=ORIENTED_EDGE('',*,*,#7096,.T.);
#4878=ORIENTED_EDGE('',*,*,#7098,.F.);
#4879=ORIENTED_EDGE('',*,*,#7074,.F.);
#4880=ORIENTED_EDGE('',*,*,#7098,.T.);
#4881=ORIENTED_EDGE('',*,*,#7095,.T.);
#4882=ORIENTED_EDGE('',*,*,#7099,.T.);
#4883=ORIENTED_EDGE('',*,*,#7075,.T.);
#4884=ORIENTED_EDGE('',*,*,#7097,.T.);
#4885=ORIENTED_EDGE('',*,*,#7073,.T.);
#4886=ORIENTED_EDGE('',*,*,#7100,.T.);
#4887=ORIENTED_EDGE('',*,*,#7085,.T.);
#4888=ORIENTED_EDGE('',*,*,#7101,.T.);
#4889=ORIENTED_EDGE('',*,*,#7102,.T.);
#4890=ORIENTED_EDGE('',*,*,#7103,.F.);
#4891=ORIENTED_EDGE('',*,*,#7104,.T.);
#4892=ORIENTED_EDGE('',*,*,#7105,.T.);
#4893=ORIENTED_EDGE('',*,*,#7103,.T.);
#4894=ORIENTED_EDGE('',*,*,#7106,.T.);
#4895=ORIENTED_EDGE('',*,*,#7107,.F.);
#4896=ORIENTED_EDGE('',*,*,#7108,.T.);
#4897=ORIENTED_EDGE('',*,*,#7109,.T.);
#4898=ORIENTED_EDGE('',*,*,#7107,.T.);
#4899=ORIENTED_EDGE('',*,*,#7110,.T.);
#4900=ORIENTED_EDGE('',*,*,#7111,.T.);
#4901=ORIENTED_EDGE('',*,*,#7112,.T.);
#4902=ORIENTED_EDGE('',*,*,#7113,.F.);
#4903=ORIENTED_EDGE('',*,*,#7114,.T.);
#4904=ORIENTED_EDGE('',*,*,#7115,.T.);
#4905=ORIENTED_EDGE('',*,*,#7113,.T.);
#4906=ORIENTED_EDGE('',*,*,#7116,.T.);
#4907=ORIENTED_EDGE('',*,*,#7117,.F.);
#4908=ORIENTED_EDGE('',*,*,#7118,.T.);
#4909=ORIENTED_EDGE('',*,*,#7119,.T.);
#4910=ORIENTED_EDGE('',*,*,#7117,.T.);
#4911=ORIENTED_EDGE('',*,*,#7120,.T.);
#4912=ORIENTED_EDGE('',*,*,#7121,.T.);
#4913=ORIENTED_EDGE('',*,*,#7122,.T.);
#4914=ORIENTED_EDGE('',*,*,#7123,.F.);
#4915=ORIENTED_EDGE('',*,*,#7124,.T.);
#4916=ORIENTED_EDGE('',*,*,#7125,.T.);
#4917=ORIENTED_EDGE('',*,*,#7123,.T.);
#4918=ORIENTED_EDGE('',*,*,#7126,.T.);
#4919=ORIENTED_EDGE('',*,*,#7127,.F.);
#4920=ORIENTED_EDGE('',*,*,#7128,.T.);
#4921=ORIENTED_EDGE('',*,*,#7129,.T.);
#4922=ORIENTED_EDGE('',*,*,#7127,.T.);
#4923=ORIENTED_EDGE('',*,*,#7130,.T.);
#4924=ORIENTED_EDGE('',*,*,#7131,.T.);
#4925=ORIENTED_EDGE('',*,*,#7132,.T.);
#4926=ORIENTED_EDGE('',*,*,#7133,.F.);
#4927=ORIENTED_EDGE('',*,*,#7134,.T.);
#4928=ORIENTED_EDGE('',*,*,#7135,.T.);
#4929=ORIENTED_EDGE('',*,*,#7133,.T.);
#4930=ORIENTED_EDGE('',*,*,#7136,.T.);
#4931=ORIENTED_EDGE('',*,*,#7137,.F.);
#4932=ORIENTED_EDGE('',*,*,#7138,.T.);
#4933=ORIENTED_EDGE('',*,*,#7139,.T.);
#4934=ORIENTED_EDGE('',*,*,#7137,.T.);
#4935=ORIENTED_EDGE('',*,*,#7140,.T.);
#4936=ORIENTED_EDGE('',*,*,#7141,.T.);
#4937=ORIENTED_EDGE('',*,*,#7142,.T.);
#4938=ORIENTED_EDGE('',*,*,#7143,.F.);
#4939=ORIENTED_EDGE('',*,*,#7144,.T.);
#4940=ORIENTED_EDGE('',*,*,#7145,.T.);
#4941=ORIENTED_EDGE('',*,*,#7143,.T.);
#4942=ORIENTED_EDGE('',*,*,#7146,.T.);
#4943=ORIENTED_EDGE('',*,*,#7147,.F.);
#4944=ORIENTED_EDGE('',*,*,#7148,.T.);
#4945=ORIENTED_EDGE('',*,*,#7149,.T.);
#4946=ORIENTED_EDGE('',*,*,#7147,.T.);
#4947=ORIENTED_EDGE('',*,*,#7150,.T.);
#4948=ORIENTED_EDGE('',*,*,#7151,.T.);
#4949=ORIENTED_EDGE('',*,*,#7152,.T.);
#4950=ORIENTED_EDGE('',*,*,#7153,.F.);
#4951=ORIENTED_EDGE('',*,*,#7154,.T.);
#4952=ORIENTED_EDGE('',*,*,#7155,.T.);
#4953=ORIENTED_EDGE('',*,*,#7153,.T.);
#4954=ORIENTED_EDGE('',*,*,#7156,.T.);
#4955=ORIENTED_EDGE('',*,*,#7157,.F.);
#4956=ORIENTED_EDGE('',*,*,#7158,.T.);
#4957=ORIENTED_EDGE('',*,*,#7159,.T.);
#4958=ORIENTED_EDGE('',*,*,#7157,.T.);
#4959=ORIENTED_EDGE('',*,*,#7160,.T.);
#4960=ORIENTED_EDGE('',*,*,#7161,.T.);
#4961=ORIENTED_EDGE('',*,*,#7162,.T.);
#4962=ORIENTED_EDGE('',*,*,#7163,.F.);
#4963=ORIENTED_EDGE('',*,*,#7164,.T.);
#4964=ORIENTED_EDGE('',*,*,#7165,.T.);
#4965=ORIENTED_EDGE('',*,*,#7163,.T.);
#4966=ORIENTED_EDGE('',*,*,#7166,.T.);
#4967=ORIENTED_EDGE('',*,*,#7167,.F.);
#4968=ORIENTED_EDGE('',*,*,#7168,.T.);
#4969=ORIENTED_EDGE('',*,*,#7169,.T.);
#4970=ORIENTED_EDGE('',*,*,#7167,.T.);
#4971=ORIENTED_EDGE('',*,*,#7170,.T.);
#4972=ORIENTED_EDGE('',*,*,#7171,.T.);
#4973=ORIENTED_EDGE('',*,*,#7172,.T.);
#4974=ORIENTED_EDGE('',*,*,#7173,.F.);
#4975=ORIENTED_EDGE('',*,*,#7174,.T.);
#4976=ORIENTED_EDGE('',*,*,#7175,.T.);
#4977=ORIENTED_EDGE('',*,*,#7173,.T.);
#4978=ORIENTED_EDGE('',*,*,#7176,.T.);
#4979=ORIENTED_EDGE('',*,*,#7177,.F.);
#4980=ORIENTED_EDGE('',*,*,#7178,.T.);
#4981=ORIENTED_EDGE('',*,*,#7179,.T.);
#4982=ORIENTED_EDGE('',*,*,#7177,.T.);
#4983=ORIENTED_EDGE('',*,*,#7180,.T.);
#4984=ORIENTED_EDGE('',*,*,#7181,.T.);
#4985=ORIENTED_EDGE('',*,*,#7182,.T.);
#4986=ORIENTED_EDGE('',*,*,#7183,.F.);
#4987=ORIENTED_EDGE('',*,*,#7184,.T.);
#4988=ORIENTED_EDGE('',*,*,#7185,.T.);
#4989=ORIENTED_EDGE('',*,*,#7183,.T.);
#4990=ORIENTED_EDGE('',*,*,#7186,.T.);
#4991=ORIENTED_EDGE('',*,*,#7187,.F.);
#4992=ORIENTED_EDGE('',*,*,#7188,.T.);
#4993=ORIENTED_EDGE('',*,*,#7189,.T.);
#4994=ORIENTED_EDGE('',*,*,#7187,.T.);
#4995=ORIENTED_EDGE('',*,*,#7190,.T.);
#4996=ORIENTED_EDGE('',*,*,#7191,.T.);
#4997=ORIENTED_EDGE('',*,*,#7192,.T.);
#4998=ORIENTED_EDGE('',*,*,#7193,.F.);
#4999=ORIENTED_EDGE('',*,*,#7194,.T.);
#5000=ORIENTED_EDGE('',*,*,#7195,.T.);
#5001=ORIENTED_EDGE('',*,*,#7193,.T.);
#5002=ORIENTED_EDGE('',*,*,#7196,.T.);
#5003=ORIENTED_EDGE('',*,*,#7197,.F.);
#5004=ORIENTED_EDGE('',*,*,#7198,.T.);
#5005=ORIENTED_EDGE('',*,*,#7199,.T.);
#5006=ORIENTED_EDGE('',*,*,#7197,.T.);
#5007=ORIENTED_EDGE('',*,*,#7200,.T.);
#5008=ORIENTED_EDGE('',*,*,#7201,.T.);
#5009=ORIENTED_EDGE('',*,*,#7202,.T.);
#5010=ORIENTED_EDGE('',*,*,#7203,.F.);
#5011=ORIENTED_EDGE('',*,*,#7204,.T.);
#5012=ORIENTED_EDGE('',*,*,#7205,.T.);
#5013=ORIENTED_EDGE('',*,*,#7203,.T.);
#5014=ORIENTED_EDGE('',*,*,#7206,.T.);
#5015=ORIENTED_EDGE('',*,*,#7207,.F.);
#5016=ORIENTED_EDGE('',*,*,#7208,.T.);
#5017=ORIENTED_EDGE('',*,*,#7209,.T.);
#5018=ORIENTED_EDGE('',*,*,#7207,.T.);
#5019=ORIENTED_EDGE('',*,*,#7210,.T.);
#5020=ORIENTED_EDGE('',*,*,#7110,.F.);
#5021=ORIENTED_EDGE('',*,*,#7106,.F.);
#5022=ORIENTED_EDGE('',*,*,#7102,.F.);
#5023=ORIENTED_EDGE('',*,*,#7211,.T.);
#5024=ORIENTED_EDGE('',*,*,#7210,.F.);
#5025=ORIENTED_EDGE('',*,*,#7206,.F.);
#5026=ORIENTED_EDGE('',*,*,#7202,.F.);
#5027=ORIENTED_EDGE('',*,*,#7212,.T.);
#5028=ORIENTED_EDGE('',*,*,#7200,.F.);
#5029=ORIENTED_EDGE('',*,*,#7196,.F.);
#5030=ORIENTED_EDGE('',*,*,#7192,.F.);
#5031=ORIENTED_EDGE('',*,*,#7213,.T.);
#5032=ORIENTED_EDGE('',*,*,#7190,.F.);
#5033=ORIENTED_EDGE('',*,*,#7186,.F.);
#5034=ORIENTED_EDGE('',*,*,#7182,.F.);
#5035=ORIENTED_EDGE('',*,*,#7214,.T.);
#5036=ORIENTED_EDGE('',*,*,#7180,.F.);
#5037=ORIENTED_EDGE('',*,*,#7176,.F.);
#5038=ORIENTED_EDGE('',*,*,#7172,.F.);
#5039=ORIENTED_EDGE('',*,*,#7215,.T.);
#5040=ORIENTED_EDGE('',*,*,#7170,.F.);
#5041=ORIENTED_EDGE('',*,*,#7166,.F.);
#5042=ORIENTED_EDGE('',*,*,#7162,.F.);
#5043=ORIENTED_EDGE('',*,*,#7216,.T.);
#5044=ORIENTED_EDGE('',*,*,#7160,.F.);
#5045=ORIENTED_EDGE('',*,*,#7156,.F.);
#5046=ORIENTED_EDGE('',*,*,#7152,.F.);
#5047=ORIENTED_EDGE('',*,*,#7217,.T.);
#5048=ORIENTED_EDGE('',*,*,#7150,.F.);
#5049=ORIENTED_EDGE('',*,*,#7146,.F.);
#5050=ORIENTED_EDGE('',*,*,#7142,.F.);
#5051=ORIENTED_EDGE('',*,*,#7218,.T.);
#5052=ORIENTED_EDGE('',*,*,#7140,.F.);
#5053=ORIENTED_EDGE('',*,*,#7136,.F.);
#5054=ORIENTED_EDGE('',*,*,#7132,.F.);
#5055=ORIENTED_EDGE('',*,*,#7219,.T.);
#5056=ORIENTED_EDGE('',*,*,#7130,.F.);
#5057=ORIENTED_EDGE('',*,*,#7126,.F.);
#5058=ORIENTED_EDGE('',*,*,#7122,.F.);
#5059=ORIENTED_EDGE('',*,*,#7220,.T.);
#5060=ORIENTED_EDGE('',*,*,#7120,.F.);
#5061=ORIENTED_EDGE('',*,*,#7116,.F.);
#5062=ORIENTED_EDGE('',*,*,#7112,.F.);
#5063=ORIENTED_EDGE('',*,*,#7221,.T.);
#5064=ORIENTED_EDGE('',*,*,#7222,.F.);
#5065=ORIENTED_EDGE('',*,*,#7105,.F.);
#5066=ORIENTED_EDGE('',*,*,#7109,.F.);
#5067=ORIENTED_EDGE('',*,*,#7223,.F.);
#5068=ORIENTED_EDGE('',*,*,#7114,.F.);
#5069=ORIENTED_EDGE('',*,*,#7115,.F.);
#5070=ORIENTED_EDGE('',*,*,#7119,.F.);
#5071=ORIENTED_EDGE('',*,*,#7224,.F.);
#5072=ORIENTED_EDGE('',*,*,#7124,.F.);
#5073=ORIENTED_EDGE('',*,*,#7125,.F.);
#5074=ORIENTED_EDGE('',*,*,#7129,.F.);
#5075=ORIENTED_EDGE('',*,*,#7225,.F.);
#5076=ORIENTED_EDGE('',*,*,#7134,.F.);
#5077=ORIENTED_EDGE('',*,*,#7135,.F.);
#5078=ORIENTED_EDGE('',*,*,#7139,.F.);
#5079=ORIENTED_EDGE('',*,*,#7226,.F.);
#5080=ORIENTED_EDGE('',*,*,#7144,.F.);
#5081=ORIENTED_EDGE('',*,*,#7145,.F.);
#5082=ORIENTED_EDGE('',*,*,#7149,.F.);
#5083=ORIENTED_EDGE('',*,*,#7227,.F.);
#5084=ORIENTED_EDGE('',*,*,#7154,.F.);
#5085=ORIENTED_EDGE('',*,*,#7155,.F.);
#5086=ORIENTED_EDGE('',*,*,#7159,.F.);
#5087=ORIENTED_EDGE('',*,*,#7228,.F.);
#5088=ORIENTED_EDGE('',*,*,#7164,.F.);
#5089=ORIENTED_EDGE('',*,*,#7165,.F.);
#5090=ORIENTED_EDGE('',*,*,#7169,.F.);
#5091=ORIENTED_EDGE('',*,*,#7229,.F.);
#5092=ORIENTED_EDGE('',*,*,#7174,.F.);
#5093=ORIENTED_EDGE('',*,*,#7175,.F.);
#5094=ORIENTED_EDGE('',*,*,#7179,.F.);
#5095=ORIENTED_EDGE('',*,*,#7230,.F.);
#5096=ORIENTED_EDGE('',*,*,#7184,.F.);
#5097=ORIENTED_EDGE('',*,*,#7185,.F.);
#5098=ORIENTED_EDGE('',*,*,#7189,.F.);
#5099=ORIENTED_EDGE('',*,*,#7231,.F.);
#5100=ORIENTED_EDGE('',*,*,#7194,.F.);
#5101=ORIENTED_EDGE('',*,*,#7195,.F.);
#5102=ORIENTED_EDGE('',*,*,#7199,.F.);
#5103=ORIENTED_EDGE('',*,*,#7232,.F.);
#5104=ORIENTED_EDGE('',*,*,#7204,.F.);
#5105=ORIENTED_EDGE('',*,*,#7205,.F.);
#5106=ORIENTED_EDGE('',*,*,#7209,.F.);
#5107=ORIENTED_EDGE('',*,*,#7233,.F.);
#5108=ORIENTED_EDGE('',*,*,#7104,.F.);
#5109=ORIENTED_EDGE('',*,*,#7234,.T.);
#5110=ORIENTED_EDGE('',*,*,#7101,.F.);
#5111=ORIENTED_EDGE('',*,*,#7233,.T.);
#5112=ORIENTED_EDGE('',*,*,#7208,.F.);
#5113=ORIENTED_EDGE('',*,*,#7211,.F.);
#5114=ORIENTED_EDGE('',*,*,#7235,.F.);
#5115=ORIENTED_EDGE('',*,*,#7236,.T.);
#5116=ORIENTED_EDGE('',*,*,#7198,.F.);
#5117=ORIENTED_EDGE('',*,*,#7212,.F.);
#5118=ORIENTED_EDGE('',*,*,#7201,.F.);
#5119=ORIENTED_EDGE('',*,*,#7232,.T.);
#5120=ORIENTED_EDGE('',*,*,#7188,.F.);
#5121=ORIENTED_EDGE('',*,*,#7213,.F.);
#5122=ORIENTED_EDGE('',*,*,#7191,.F.);
#5123=ORIENTED_EDGE('',*,*,#7231,.T.);
#5124=ORIENTED_EDGE('',*,*,#7178,.F.);
#5125=ORIENTED_EDGE('',*,*,#7214,.F.);
#5126=ORIENTED_EDGE('',*,*,#7181,.F.);
#5127=ORIENTED_EDGE('',*,*,#7230,.T.);
#5128=ORIENTED_EDGE('',*,*,#7168,.F.);
#5129=ORIENTED_EDGE('',*,*,#7215,.F.);
#5130=ORIENTED_EDGE('',*,*,#7171,.F.);
#5131=ORIENTED_EDGE('',*,*,#7229,.T.);
#5132=ORIENTED_EDGE('',*,*,#7158,.F.);
#5133=ORIENTED_EDGE('',*,*,#7216,.F.);
#5134=ORIENTED_EDGE('',*,*,#7161,.F.);
#5135=ORIENTED_EDGE('',*,*,#7228,.T.);
#5136=ORIENTED_EDGE('',*,*,#7148,.F.);
#5137=ORIENTED_EDGE('',*,*,#7217,.F.);
#5138=ORIENTED_EDGE('',*,*,#7151,.F.);
#5139=ORIENTED_EDGE('',*,*,#7227,.T.);
#5140=ORIENTED_EDGE('',*,*,#7138,.F.);
#5141=ORIENTED_EDGE('',*,*,#7218,.F.);
#5142=ORIENTED_EDGE('',*,*,#7141,.F.);
#5143=ORIENTED_EDGE('',*,*,#7226,.T.);
#5144=ORIENTED_EDGE('',*,*,#7128,.F.);
#5145=ORIENTED_EDGE('',*,*,#7219,.F.);
#5146=ORIENTED_EDGE('',*,*,#7131,.F.);
#5147=ORIENTED_EDGE('',*,*,#7225,.T.);
#5148=ORIENTED_EDGE('',*,*,#7118,.F.);
#5149=ORIENTED_EDGE('',*,*,#7220,.F.);
#5150=ORIENTED_EDGE('',*,*,#7121,.F.);
#5151=ORIENTED_EDGE('',*,*,#7224,.T.);
#5152=ORIENTED_EDGE('',*,*,#7108,.F.);
#5153=ORIENTED_EDGE('',*,*,#7221,.F.);
#5154=ORIENTED_EDGE('',*,*,#7111,.F.);
#5155=ORIENTED_EDGE('',*,*,#7223,.T.);
#5156=ORIENTED_EDGE('',*,*,#7079,.T.);
#5157=ORIENTED_EDGE('',*,*,#7078,.T.);
#5158=ORIENTED_EDGE('',*,*,#7077,.T.);
#5159=ORIENTED_EDGE('',*,*,#7076,.T.);
#5160=ORIENTED_EDGE('',*,*,#7099,.F.);
#5161=ORIENTED_EDGE('',*,*,#7094,.F.);
#5162=ORIENTED_EDGE('',*,*,#7093,.F.);
#5163=ORIENTED_EDGE('',*,*,#7092,.F.);
#5164=ORIENTED_EDGE('',*,*,#7091,.F.);
#5165=ORIENTED_EDGE('',*,*,#7090,.F.);
#5166=ORIENTED_EDGE('',*,*,#7089,.F.);
#5167=ORIENTED_EDGE('',*,*,#7088,.F.);
#5168=ORIENTED_EDGE('',*,*,#7087,.F.);
#5169=ORIENTED_EDGE('',*,*,#7086,.F.);
#5170=ORIENTED_EDGE('',*,*,#7234,.F.);
#5171=ORIENTED_EDGE('',*,*,#7100,.F.);
#5172=ORIENTED_EDGE('',*,*,#7084,.T.);
#5173=ORIENTED_EDGE('',*,*,#7083,.T.);
#5174=ORIENTED_EDGE('',*,*,#7082,.T.);
#5175=ORIENTED_EDGE('',*,*,#7081,.T.);
#5176=ORIENTED_EDGE('',*,*,#7080,.T.);
#5177=ORIENTED_EDGE('',*,*,#7235,.T.);
#5178=ORIENTED_EDGE('',*,*,#7222,.T.);
#5179=ORIENTED_EDGE('',*,*,#7236,.F.);
#7073=EDGE_CURVE('',#8504,#8505,#9415,.T.);
#7074=EDGE_CURVE('',#8504,#8506,#1929,.T.);
#7075=EDGE_CURVE('',#8507,#8506,#9416,.T.);
#7076=EDGE_CURVE('',#8508,#8507,#1930,.T.);
#7077=EDGE_CURVE('',#8509,#8508,#1931,.T.);
#7078=EDGE_CURVE('',#8510,#8509,#1932,.T.);
#7079=EDGE_CURVE('',#8511,#8510,#1933,.T.);
#7080=EDGE_CURVE('',#8512,#8511,#1934,.T.);
#7081=EDGE_CURVE('',#8513,#8512,#1935,.T.);
#7082=EDGE_CURVE('',#8514,#8513,#1936,.T.);
#7083=EDGE_CURVE('',#8515,#8514,#1937,.T.);
#7084=EDGE_CURVE('',#8505,#8515,#1938,.T.);
#7085=EDGE_CURVE('',#8516,#8517,#9417,.T.);
#7086=EDGE_CURVE('',#8516,#8518,#1939,.T.);
#7087=EDGE_CURVE('',#8518,#8519,#1940,.T.);
#7088=EDGE_CURVE('',#8519,#8520,#1941,.T.);
#7089=EDGE_CURVE('',#8520,#8521,#1942,.T.);
#7090=EDGE_CURVE('',#8521,#8522,#1943,.T.);
#7091=EDGE_CURVE('',#8522,#8523,#1944,.T.);
#7092=EDGE_CURVE('',#8523,#8524,#1945,.T.);
#7093=EDGE_CURVE('',#8524,#8525,#1946,.T.);
#7094=EDGE_CURVE('',#8525,#8526,#1147,.T.);
#7095=EDGE_CURVE('',#8527,#8526,#9418,.T.);
#7096=EDGE_CURVE('',#8517,#8527,#1947,.T.);
#7097=EDGE_CURVE('',#8517,#8504,#9419,.T.);
#7098=EDGE_CURVE('',#8506,#8527,#9420,.T.);
#7099=EDGE_CURVE('',#8526,#8507,#9421,.T.);
#7100=EDGE_CURVE('',#8505,#8516,#9422,.T.);
#7101=EDGE_CURVE('',#8528,#8529,#9423,.T.);
#7102=EDGE_CURVE('',#8529,#8530,#9424,.T.);
#7103=EDGE_CURVE('',#8531,#8530,#9425,.T.);
#7104=EDGE_CURVE('',#8531,#8528,#9426,.T.);
#7105=EDGE_CURVE('',#8532,#8531,#9427,.T.);
#7106=EDGE_CURVE('',#8530,#8533,#9428,.T.);
#7107=EDGE_CURVE('',#8532,#8533,#9429,.T.);
#7108=EDGE_CURVE('',#8534,#8535,#9430,.T.);
#7109=EDGE_CURVE('',#8535,#8532,#9431,.T.);
#7110=EDGE_CURVE('',#8533,#8534,#9432,.T.);
#7111=EDGE_CURVE('',#8536,#8537,#9433,.T.);
#7112=EDGE_CURVE('',#8537,#8538,#9434,.T.);
#7113=EDGE_CURVE('',#8539,#8538,#9435,.T.);
#7114=EDGE_CURVE('',#8539,#8536,#9436,.T.);
#7115=EDGE_CURVE('',#8540,#8539,#9437,.T.);
#7116=EDGE_CURVE('',#8538,#8541,#9438,.T.);
#7117=EDGE_CURVE('',#8540,#8541,#9439,.T.);
#7118=EDGE_CURVE('',#8542,#8543,#9440,.T.);
#7119=EDGE_CURVE('',#8543,#8540,#9441,.T.);
#7120=EDGE_CURVE('',#8541,#8542,#9442,.T.);
#7121=EDGE_CURVE('',#8544,#8545,#9443,.T.);
#7122=EDGE_CURVE('',#8545,#8546,#9444,.T.);
#7123=EDGE_CURVE('',#8547,#8546,#9445,.T.);
#7124=EDGE_CURVE('',#8547,#8544,#9446,.T.);
#7125=EDGE_CURVE('',#8548,#8547,#9447,.T.);
#7126=EDGE_CURVE('',#8546,#8549,#9448,.T.);
#7127=EDGE_CURVE('',#8548,#8549,#9449,.T.);
#7128=EDGE_CURVE('',#8550,#8551,#9450,.T.);
#7129=EDGE_CURVE('',#8551,#8548,#9451,.T.);
#7130=EDGE_CURVE('',#8549,#8550,#9452,.T.);
#7131=EDGE_CURVE('',#8552,#8553,#9453,.T.);
#7132=EDGE_CURVE('',#8553,#8554,#9454,.T.);
#7133=EDGE_CURVE('',#8555,#8554,#9455,.T.);
#7134=EDGE_CURVE('',#8555,#8552,#9456,.T.);
#7135=EDGE_CURVE('',#8556,#8555,#9457,.T.);
#7136=EDGE_CURVE('',#8554,#8557,#9458,.T.);
#7137=EDGE_CURVE('',#8556,#8557,#9459,.T.);
#7138=EDGE_CURVE('',#8558,#8559,#9460,.T.);
#7139=EDGE_CURVE('',#8559,#8556,#9461,.T.);
#7140=EDGE_CURVE('',#8557,#8558,#9462,.T.);
#7141=EDGE_CURVE('',#8560,#8561,#9463,.T.);
#7142=EDGE_CURVE('',#8561,#8562,#9464,.T.);
#7143=EDGE_CURVE('',#8563,#8562,#9465,.T.);
#7144=EDGE_CURVE('',#8563,#8560,#9466,.T.);
#7145=EDGE_CURVE('',#8564,#8563,#9467,.T.);
#7146=EDGE_CURVE('',#8562,#8565,#9468,.T.);
#7147=EDGE_CURVE('',#8564,#8565,#9469,.T.);
#7148=EDGE_CURVE('',#8566,#8567,#9470,.T.);
#7149=EDGE_CURVE('',#8567,#8564,#9471,.T.);
#7150=EDGE_CURVE('',#8565,#8566,#9472,.T.);
#7151=EDGE_CURVE('',#8568,#8569,#9473,.T.);
#7152=EDGE_CURVE('',#8569,#8570,#9474,.T.);
#7153=EDGE_CURVE('',#8571,#8570,#9475,.T.);
#7154=EDGE_CURVE('',#8571,#8568,#9476,.T.);
#7155=EDGE_CURVE('',#8572,#8571,#9477,.T.);
#7156=EDGE_CURVE('',#8570,#8573,#9478,.T.);
#7157=EDGE_CURVE('',#8572,#8573,#9479,.T.);
#7158=EDGE_CURVE('',#8574,#8575,#9480,.T.);
#7159=EDGE_CURVE('',#8575,#8572,#9481,.T.);
#7160=EDGE_CURVE('',#8573,#8574,#9482,.T.);
#7161=EDGE_CURVE('',#8576,#8577,#9483,.T.);
#7162=EDGE_CURVE('',#8577,#8578,#9484,.T.);
#7163=EDGE_CURVE('',#8579,#8578,#9485,.T.);
#7164=EDGE_CURVE('',#8579,#8576,#9486,.T.);
#7165=EDGE_CURVE('',#8580,#8579,#9487,.T.);
#7166=EDGE_CURVE('',#8578,#8581,#9488,.T.);
#7167=EDGE_CURVE('',#8580,#8581,#9489,.T.);
#7168=EDGE_CURVE('',#8582,#8583,#9490,.T.);
#7169=EDGE_CURVE('',#8583,#8580,#9491,.T.);
#7170=EDGE_CURVE('',#8581,#8582,#9492,.T.);
#7171=EDGE_CURVE('',#8584,#8585,#9493,.T.);
#7172=EDGE_CURVE('',#8585,#8586,#9494,.T.);
#7173=EDGE_CURVE('',#8587,#8586,#9495,.T.);
#7174=EDGE_CURVE('',#8587,#8584,#9496,.T.);
#7175=EDGE_CURVE('',#8588,#8587,#9497,.T.);
#7176=EDGE_CURVE('',#8586,#8589,#9498,.T.);
#7177=EDGE_CURVE('',#8588,#8589,#9499,.T.);
#7178=EDGE_CURVE('',#8590,#8591,#9500,.T.);
#7179=EDGE_CURVE('',#8591,#8588,#9501,.T.);
#7180=EDGE_CURVE('',#8589,#8590,#9502,.T.);
#7181=EDGE_CURVE('',#8592,#8593,#9503,.T.);
#7182=EDGE_CURVE('',#8593,#8594,#9504,.T.);
#7183=EDGE_CURVE('',#8595,#8594,#9505,.T.);
#7184=EDGE_CURVE('',#8595,#8592,#9506,.T.);
#7185=EDGE_CURVE('',#8596,#8595,#9507,.T.);
#7186=EDGE_CURVE('',#8594,#8597,#9508,.T.);
#7187=EDGE_CURVE('',#8596,#8597,#9509,.T.);
#7188=EDGE_CURVE('',#8598,#8599,#9510,.T.);
#7189=EDGE_CURVE('',#8599,#8596,#9511,.T.);
#7190=EDGE_CURVE('',#8597,#8598,#9512,.T.);
#7191=EDGE_CURVE('',#8600,#8601,#9513,.T.);
#7192=EDGE_CURVE('',#8601,#8602,#9514,.T.);
#7193=EDGE_CURVE('',#8603,#8602,#9515,.T.);
#7194=EDGE_CURVE('',#8603,#8600,#9516,.T.);
#7195=EDGE_CURVE('',#8604,#8603,#9517,.T.);
#7196=EDGE_CURVE('',#8602,#8605,#9518,.T.);
#7197=EDGE_CURVE('',#8604,#8605,#9519,.T.);
#7198=EDGE_CURVE('',#8606,#8607,#9520,.T.);
#7199=EDGE_CURVE('',#8607,#8604,#9521,.T.);
#7200=EDGE_CURVE('',#8605,#8606,#9522,.T.);
#7201=EDGE_CURVE('',#8608,#8609,#9523,.T.);
#7202=EDGE_CURVE('',#8609,#8610,#9524,.T.);
#7203=EDGE_CURVE('',#8611,#8610,#9525,.T.);
#7204=EDGE_CURVE('',#8611,#8608,#9526,.T.);
#7205=EDGE_CURVE('',#8612,#8611,#9527,.T.);
#7206=EDGE_CURVE('',#8610,#8613,#9528,.T.);
#7207=EDGE_CURVE('',#8612,#8613,#9529,.T.);
#7208=EDGE_CURVE('',#8614,#8615,#9530,.T.);
#7209=EDGE_CURVE('',#8615,#8612,#9531,.T.);
#7210=EDGE_CURVE('',#8613,#8614,#9532,.T.);
#7211=EDGE_CURVE('',#8529,#8614,#950,.T.);
#7212=EDGE_CURVE('',#8609,#8606,#951,.T.);
#7213=EDGE_CURVE('',#8601,#8598,#952,.T.);
#7214=EDGE_CURVE('',#8593,#8590,#953,.T.);
#7215=EDGE_CURVE('',#8585,#8582,#954,.T.);
#7216=EDGE_CURVE('',#8577,#8574,#955,.T.);
#7217=EDGE_CURVE('',#8569,#8566,#956,.T.);
#7218=EDGE_CURVE('',#8561,#8558,#957,.T.);
#7219=EDGE_CURVE('',#8553,#8550,#958,.T.);
#7220=EDGE_CURVE('',#8545,#8542,#959,.T.);
#7221=EDGE_CURVE('',#8537,#8534,#960,.T.);
#7222=EDGE_CURVE('',#8616,#8616,#961,.T.);
#7223=EDGE_CURVE('',#8536,#8535,#962,.T.);
#7224=EDGE_CURVE('',#8544,#8543,#963,.T.);
#7225=EDGE_CURVE('',#8552,#8551,#964,.T.);
#7226=EDGE_CURVE('',#8560,#8559,#965,.T.);
#7227=EDGE_CURVE('',#8568,#8567,#966,.T.);
#7228=EDGE_CURVE('',#8576,#8575,#967,.T.);
#7229=EDGE_CURVE('',#8584,#8583,#968,.T.);
#7230=EDGE_CURVE('',#8592,#8591,#969,.T.);
#7231=EDGE_CURVE('',#8600,#8599,#970,.T.);
#7232=EDGE_CURVE('',#8608,#8607,#971,.T.);
#7233=EDGE_CURVE('',#8528,#8615,#972,.T.);
#7234=EDGE_CURVE('',#8516,#8516,#973,.T.);
#7235=EDGE_CURVE('',#8617,#8617,#974,.T.);
#7236=EDGE_CURVE('',#8618,#8618,#975,.T.);
#8504=VERTEX_POINT('',#39730);
#8505=VERTEX_POINT('',#39731);
#8506=VERTEX_POINT('',#39811);
#8507=VERTEX_POINT('',#39813);
#8508=VERTEX_POINT('',#39819);
#8509=VERTEX_POINT('',#39833);
#8510=VERTEX_POINT('',#39847);
#8511=VERTEX_POINT('',#39861);
#8512=VERTEX_POINT('',#39875);
#8513=VERTEX_POINT('',#39889);
#8514=VERTEX_POINT('',#39903);
#8515=VERTEX_POINT('',#39917);
#8516=VERTEX_POINT('',#40169);
#8517=VERTEX_POINT('',#40170);
#8518=VERTEX_POINT('',#40178);
#8519=VERTEX_POINT('',#40192);
#8520=VERTEX_POINT('',#40206);
#8521=VERTEX_POINT('',#40220);
#8522=VERTEX_POINT('',#40234);
#8523=VERTEX_POINT('',#40248);
#8524=VERTEX_POINT('',#40262);
#8525=VERTEX_POINT('',#40276);
#8526=VERTEX_POINT('',#40281);
#8527=VERTEX_POINT('',#40283);
#8528=VERTEX_POINT('',#40827);
#8529=VERTEX_POINT('',#40828);
#8530=VERTEX_POINT('',#40830);
#8531=VERTEX_POINT('',#40832);
#8532=VERTEX_POINT('',#40836);
#8533=VERTEX_POINT('',#40838);
#8534=VERTEX_POINT('',#40842);
#8535=VERTEX_POINT('',#40843);
#8536=VERTEX_POINT('',#40848);
#8537=VERTEX_POINT('',#40849);
#8538=VERTEX_POINT('',#40851);
#8539=VERTEX_POINT('',#40853);
#8540=VERTEX_POINT('',#40857);
#8541=VERTEX_POINT('',#40859);
#8542=VERTEX_POINT('',#40863);
#8543=VERTEX_POINT('',#40864);
#8544=VERTEX_POINT('',#40869);
#8545=VERTEX_POINT('',#40870);
#8546=VERTEX_POINT('',#40872);
#8547=VERTEX_POINT('',#40874);
#8548=VERTEX_POINT('',#40878);
#8549=VERTEX_POINT('',#40880);
#8550=VERTEX_POINT('',#40884);
#8551=VERTEX_POINT('',#40885);
#8552=VERTEX_POINT('',#40890);
#8553=VERTEX_POINT('',#40891);
#8554=VERTEX_POINT('',#40893);
#8555=VERTEX_POINT('',#40895);
#8556=VERTEX_POINT('',#40899);
#8557=VERTEX_POINT('',#40901);
#8558=VERTEX_POINT('',#40905);
#8559=VERTEX_POINT('',#40906);
#8560=VERTEX_POINT('',#40911);
#8561=VERTEX_POINT('',#40912);
#8562=VERTEX_POINT('',#40914);
#8563=VERTEX_POINT('',#40916);
#8564=VERTEX_POINT('',#40920);
#8565=VERTEX_POINT('',#40922);
#8566=VERTEX_POINT('',#40926);
#8567=VERTEX_POINT('',#40927);
#8568=VERTEX_POINT('',#40932);
#8569=VERTEX_POINT('',#40933);
#8570=VERTEX_POINT('',#40935);
#8571=VERTEX_POINT('',#40937);
#8572=VERTEX_POINT('',#40941);
#8573=VERTEX_POINT('',#40943);
#8574=VERTEX_POINT('',#40947);
#8575=VERTEX_POINT('',#40948);
#8576=VERTEX_POINT('',#40953);
#8577=VERTEX_POINT('',#40954);
#8578=VERTEX_POINT('',#40956);
#8579=VERTEX_POINT('',#40958);
#8580=VERTEX_POINT('',#40962);
#8581=VERTEX_POINT('',#40964);
#8582=VERTEX_POINT('',#40968);
#8583=VERTEX_POINT('',#40969);
#8584=VERTEX_POINT('',#40974);
#8585=VERTEX_POINT('',#40975);
#8586=VERTEX_POINT('',#40977);
#8587=VERTEX_POINT('',#40979);
#8588=VERTEX_POINT('',#40983);
#8589=VERTEX_POINT('',#40985);
#8590=VERTEX_POINT('',#40989);
#8591=VERTEX_POINT('',#40990);
#8592=VERTEX_POINT('',#40995);
#8593=VERTEX_POINT('',#40996);
#8594=VERTEX_POINT('',#40998);
#8595=VERTEX_POINT('',#41000);
#8596=VERTEX_POINT('',#41004);
#8597=VERTEX_POINT('',#41006);
#8598=VERTEX_POINT('',#41010);
#8599=VERTEX_POINT('',#41011);
#8600=VERTEX_POINT('',#41016);
#8601=VERTEX_POINT('',#41017);
#8602=VERTEX_POINT('',#41019);
#8603=VERTEX_POINT('',#41021);
#8604=VERTEX_POINT('',#41025);
#8605=VERTEX_POINT('',#41027);
#8606=VERTEX_POINT('',#41031);
#8607=VERTEX_POINT('',#41032);
#8608=VERTEX_POINT('',#41037);
#8609=VERTEX_POINT('',#41038);
#8610=VERTEX_POINT('',#41040);
#8611=VERTEX_POINT('',#41042);
#8612=VERTEX_POINT('',#41046);
#8613=VERTEX_POINT('',#41048);
#8614=VERTEX_POINT('',#41052);
#8615=VERTEX_POINT('',#41053);
#8616=VERTEX_POINT('',#41069);
#8617=VERTEX_POINT('',#41086);
#8618=VERTEX_POINT('',#41088);
#9415=LINE('',#39729,#10243);
#9416=LINE('',#39812,#10244);
#9417=LINE('',#40168,#10245);
#9418=LINE('',#40282,#10246);
#9419=LINE('',#40819,#10247);
#9420=LINE('',#40820,#10248);
#9421=LINE('',#40822,#10249);
#9422=LINE('',#40824,#10250);
#9423=LINE('',#40826,#10251);
#9424=LINE('',#40829,#10252);
#9425=LINE('',#40831,#10253);
#9426=LINE('',#40833,#10254);
#9427=LINE('',#40835,#10255);
#9428=LINE('',#40837,#10256);
#9429=LINE('',#40839,#10257);
#9430=LINE('',#40841,#10258);
#9431=LINE('',#40844,#10259);
#9432=LINE('',#40845,#10260);
#9433=LINE('',#40847,#10261);
#9434=LINE('',#40850,#10262);
#9435=LINE('',#40852,#10263);
#9436=LINE('',#40854,#10264);
#9437=LINE('',#40856,#10265);
#9438=LINE('',#40858,#10266);
#9439=LINE('',#40860,#10267);
#9440=LINE('',#40862,#10268);
#9441=LINE('',#40865,#10269);
#9442=LINE('',#40866,#10270);
#9443=LINE('',#40868,#10271);
#9444=LINE('',#40871,#10272);
#9445=LINE('',#40873,#10273);
#9446=LINE('',#40875,#10274);
#9447=LINE('',#40877,#10275);
#9448=LINE('',#40879,#10276);
#9449=LINE('',#40881,#10277);
#9450=LINE('',#40883,#10278);
#9451=LINE('',#40886,#10279);
#9452=LINE('',#40887,#10280);
#9453=LINE('',#40889,#10281);
#9454=LINE('',#40892,#10282);
#9455=LINE('',#40894,#10283);
#9456=LINE('',#40896,#10284);
#9457=LINE('',#40898,#10285);
#9458=LINE('',#40900,#10286);
#9459=LINE('',#40902,#10287);
#9460=LINE('',#40904,#10288);
#9461=LINE('',#40907,#10289);
#9462=LINE('',#40908,#10290);
#9463=LINE('',#40910,#10291);
#9464=LINE('',#40913,#10292);
#9465=LINE('',#40915,#10293);
#9466=LINE('',#40917,#10294);
#9467=LINE('',#40919,#10295);
#9468=LINE('',#40921,#10296);
#9469=LINE('',#40923,#10297);
#9470=LINE('',#40925,#10298);
#9471=LINE('',#40928,#10299);
#9472=LINE('',#40929,#10300);
#9473=LINE('',#40931,#10301);
#9474=LINE('',#40934,#10302);
#9475=LINE('',#40936,#10303);
#9476=LINE('',#40938,#10304);
#9477=LINE('',#40940,#10305);
#9478=LINE('',#40942,#10306);
#9479=LINE('',#40944,#10307);
#9480=LINE('',#40946,#10308);
#9481=LINE('',#40949,#10309);
#9482=LINE('',#40950,#10310);
#9483=LINE('',#40952,#10311);
#9484=LINE('',#40955,#10312);
#9485=LINE('',#40957,#10313);
#9486=LINE('',#40959,#10314);
#9487=LINE('',#40961,#10315);
#9488=LINE('',#40963,#10316);
#9489=LINE('',#40965,#10317);
#9490=LINE('',#40967,#10318);
#9491=LINE('',#40970,#10319);
#9492=LINE('',#40971,#10320);
#9493=LINE('',#40973,#10321);
#9494=LINE('',#40976,#10322);
#9495=LINE('',#40978,#10323);
#9496=LINE('',#40980,#10324);
#9497=LINE('',#40982,#10325);
#9498=LINE('',#40984,#10326);
#9499=LINE('',#40986,#10327);
#9500=LINE('',#40988,#10328);
#9501=LINE('',#40991,#10329);
#9502=LINE('',#40992,#10330);
#9503=LINE('',#40994,#10331);
#9504=LINE('',#40997,#10332);
#9505=LINE('',#40999,#10333);
#9506=LINE('',#41001,#10334);
#9507=LINE('',#41003,#10335);
#9508=LINE('',#41005,#10336);
#9509=LINE('',#41007,#10337);
#9510=LINE('',#41009,#10338);
#9511=LINE('',#41012,#10339);
#9512=LINE('',#41013,#10340);
#9513=LINE('',#41015,#10341);
#9514=LINE('',#41018,#10342);
#9515=LINE('',#41020,#10343);
#9516=LINE('',#41022,#10344);
#9517=LINE('',#41024,#10345);
#9518=LINE('',#41026,#10346);
#9519=LINE('',#41028,#10347);
#9520=LINE('',#41030,#10348);
#9521=LINE('',#41033,#10349);
#9522=LINE('',#41034,#10350);
#9523=LINE('',#41036,#10351);
#9524=LINE('',#41039,#10352);
#9525=LINE('',#41041,#10353);
#9526=LINE('',#41043,#10354);
#9527=LINE('',#41045,#10355);
#9528=LINE('',#41047,#10356);
#9529=LINE('',#41049,#10357);
#9530=LINE('',#41051,#10358);
#9531=LINE('',#41054,#10359);
#9532=LINE('',#41055,#10360);
#10243=VECTOR('',#18431,1.);
#10244=VECTOR('',#18432,1.);
#10245=VECTOR('',#18433,1.);
#10246=VECTOR('',#18434,1.);
#10247=VECTOR('',#18435,1.);
#10248=VECTOR('',#18436,1.);
#10249=VECTOR('',#18439,1.);
#10250=VECTOR('',#18442,1.);
#10251=VECTOR('',#18445,1.);
#10252=VECTOR('',#18446,1.);
#10253=VECTOR('',#18447,1.);
#10254=VECTOR('',#18448,1.);
#10255=VECTOR('',#18451,1.);
#10256=VECTOR('',#18452,1.);
#10257=VECTOR('',#18453,1.);
#10258=VECTOR('',#18456,1.);
#10259=VECTOR('',#18457,1.);
#10260=VECTOR('',#18458,1.);
#10261=VECTOR('',#18461,1.);
#10262=VECTOR('',#18462,1.);
#10263=VECTOR('',#18463,1.);
#10264=VECTOR('',#18464,1.);
#10265=VECTOR('',#18467,1.);
#10266=VECTOR('',#18468,1.);
#10267=VECTOR('',#18469,1.);
#10268=VECTOR('',#18472,1.);
#10269=VECTOR('',#18473,1.);
#10270=VECTOR('',#18474,1.);
#10271=VECTOR('',#18477,1.);
#10272=VECTOR('',#18478,1.);
#10273=VECTOR('',#18479,1.);
#10274=VECTOR('',#18480,1.);
#10275=VECTOR('',#18483,1.);
#10276=VECTOR('',#18484,1.);
#10277=VECTOR('',#18485,1.);
#10278=VECTOR('',#18488,1.);
#10279=VECTOR('',#18489,1.);
#10280=VECTOR('',#18490,1.);
#10281=VECTOR('',#18493,1.);
#10282=VECTOR('',#18494,1.);
#10283=VECTOR('',#18495,1.);
#10284=VECTOR('',#18496,1.);
#10285=VECTOR('',#18499,1.);
#10286=VECTOR('',#18500,1.);
#10287=VECTOR('',#18501,1.);
#10288=VECTOR('',#18504,1.);
#10289=VECTOR('',#18505,1.);
#10290=VECTOR('',#18506,1.);
#10291=VECTOR('',#18509,1.);
#10292=VECTOR('',#18510,1.);
#10293=VECTOR('',#18511,1.);
#10294=VECTOR('',#18512,1.);
#10295=VECTOR('',#18515,1.);
#10296=VECTOR('',#18516,1.);
#10297=VECTOR('',#18517,1.);
#10298=VECTOR('',#18520,1.);
#10299=VECTOR('',#18521,1.);
#10300=VECTOR('',#18522,1.);
#10301=VECTOR('',#18525,1.);
#10302=VECTOR('',#18526,1.);
#10303=VECTOR('',#18527,1.);
#10304=VECTOR('',#18528,1.);
#10305=VECTOR('',#18531,1.);
#10306=VECTOR('',#18532,1.);
#10307=VECTOR('',#18533,1.);
#10308=VECTOR('',#18536,1.);
#10309=VECTOR('',#18537,1.);
#10310=VECTOR('',#18538,1.);
#10311=VECTOR('',#18541,1.);
#10312=VECTOR('',#18542,1.);
#10313=VECTOR('',#18543,1.);
#10314=VECTOR('',#18544,1.);
#10315=VECTOR('',#18547,1.);
#10316=VECTOR('',#18548,1.);
#10317=VECTOR('',#18549,1.);
#10318=VECTOR('',#18552,1.);
#10319=VECTOR('',#18553,1.);
#10320=VECTOR('',#18554,1.);
#10321=VECTOR('',#18557,1.);
#10322=VECTOR('',#18558,1.);
#10323=VECTOR('',#18559,1.);
#10324=VECTOR('',#18560,1.);
#10325=VECTOR('',#18563,1.);
#10326=VECTOR('',#18564,1.);
#10327=VECTOR('',#18565,1.);
#10328=VECTOR('',#18568,1.);
#10329=VECTOR('',#18569,1.);
#10330=VECTOR('',#18570,1.);
#10331=VECTOR('',#18573,1.);
#10332=VECTOR('',#18574,1.);
#10333=VECTOR('',#18575,1.);
#10334=VECTOR('',#18576,1.);
#10335=VECTOR('',#18579,1.);
#10336=VECTOR('',#18580,1.);
#10337=VECTOR('',#18581,1.);
#10338=VECTOR('',#18584,1.);
#10339=VECTOR('',#18585,1.);
#10340=VECTOR('',#18586,1.);
#10341=VECTOR('',#18589,1.);
#10342=VECTOR('',#18590,1.);
#10343=VECTOR('',#18591,1.);
#10344=VECTOR('',#18592,1.);
#10345=VECTOR('',#18595,1.);
#10346=VECTOR('',#18596,1.);
#10347=VECTOR('',#18597,1.);
#10348=VECTOR('',#18600,1.);
#10349=VECTOR('',#18601,1.);
#10350=VECTOR('',#18602,1.);
#10351=VECTOR('',#18605,1.);
#10352=VECTOR('',#18606,1.);
#10353=VECTOR('',#18607,1.);
#10354=VECTOR('',#18608,1.);
#10355=VECTOR('',#18611,1.);
#10356=VECTOR('',#18612,1.);
#10357=VECTOR('',#18613,1.);
#10358=VECTOR('',#18616,1.);
#10359=VECTOR('',#18617,1.);
#10360=VECTOR('',#18618,1.);
#11362=EDGE_LOOP('',(#4852,#4853,#4854,#4855,#4856,#4857,#4858,#4859,#4860,
#4861,#4862,#4863));
#11363=EDGE_LOOP('',(#4864,#4865,#4866,#4867,#4868,#4869,#4870,#4871,#4872,
#4873,#4874,#4875));
#11364=EDGE_LOOP('',(#4876,#4877,#4878,#4879));
#11365=EDGE_LOOP('',(#4880,#4881,#4882,#4883));
#11366=EDGE_LOOP('',(#4884,#4885,#4886,#4887));
#11367=EDGE_LOOP('',(#4888,#4889,#4890,#4891));
#11368=EDGE_LOOP('',(#4892,#4893,#4894,#4895));
#11369=EDGE_LOOP('',(#4896,#4897,#4898,#4899));
#11370=EDGE_LOOP('',(#4900,#4901,#4902,#4903));
#11371=EDGE_LOOP('',(#4904,#4905,#4906,#4907));
#11372=EDGE_LOOP('',(#4908,#4909,#4910,#4911));
#11373=EDGE_LOOP('',(#4912,#4913,#4914,#4915));
#11374=EDGE_LOOP('',(#4916,#4917,#4918,#4919));
#11375=EDGE_LOOP('',(#4920,#4921,#4922,#4923));
#11376=EDGE_LOOP('',(#4924,#4925,#4926,#4927));
#11377=EDGE_LOOP('',(#4928,#4929,#4930,#4931));
#11378=EDGE_LOOP('',(#4932,#4933,#4934,#4935));
#11379=EDGE_LOOP('',(#4936,#4937,#4938,#4939));
#11380=EDGE_LOOP('',(#4940,#4941,#4942,#4943));
#11381=EDGE_LOOP('',(#4944,#4945,#4946,#4947));
#11382=EDGE_LOOP('',(#4948,#4949,#4950,#4951));
#11383=EDGE_LOOP('',(#4952,#4953,#4954,#4955));
#11384=EDGE_LOOP('',(#4956,#4957,#4958,#4959));
#11385=EDGE_LOOP('',(#4960,#4961,#4962,#4963));
#11386=EDGE_LOOP('',(#4964,#4965,#4966,#4967));
#11387=EDGE_LOOP('',(#4968,#4969,#4970,#4971));
#11388=EDGE_LOOP('',(#4972,#4973,#4974,#4975));
#11389=EDGE_LOOP('',(#4976,#4977,#4978,#4979));
#11390=EDGE_LOOP('',(#4980,#4981,#4982,#4983));
#11391=EDGE_LOOP('',(#4984,#4985,#4986,#4987));
#11392=EDGE_LOOP('',(#4988,#4989,#4990,#4991));
#11393=EDGE_LOOP('',(#4992,#4993,#4994,#4995));
#11394=EDGE_LOOP('',(#4996,#4997,#4998,#4999));
#11395=EDGE_LOOP('',(#5000,#5001,#5002,#5003));
#11396=EDGE_LOOP('',(#5004,#5005,#5006,#5007));
#11397=EDGE_LOOP('',(#5008,#5009,#5010,#5011));
#11398=EDGE_LOOP('',(#5012,#5013,#5014,#5015));
#11399=EDGE_LOOP('',(#5016,#5017,#5018,#5019));
#11400=EDGE_LOOP('',(#5020,#5021,#5022,#5023,#5024,#5025,#5026,#5027,#5028,
#5029,#5030,#5031,#5032,#5033,#5034,#5035,#5036,#5037,#5038,#5039,#5040,
#5041,#5042,#5043,#5044,#5045,#5046,#5047,#5048,#5049,#5050,#5051,#5052,
#5053,#5054,#5055,#5056,#5057,#5058,#5059,#5060,#5061,#5062,#5063));
#11401=EDGE_LOOP('',(#5064));
#11402=EDGE_LOOP('',(#5065,#5066,#5067,#5068,#5069,#5070,#5071,#5072,#5073,
#5074,#5075,#5076,#5077,#5078,#5079,#5080,#5081,#5082,#5083,#5084,#5085,
#5086,#5087,#5088,#5089,#5090,#5091,#5092,#5093,#5094,#5095,#5096,#5097,
#5098,#5099,#5100,#5101,#5102,#5103,#5104,#5105,#5106,#5107,#5108));
#11403=EDGE_LOOP('',(#5109));
#11404=EDGE_LOOP('',(#5110,#5111,#5112,#5113));
#11405=EDGE_LOOP('',(#5114));
#11406=EDGE_LOOP('',(#5115));
#11407=EDGE_LOOP('',(#5116,#5117,#5118,#5119));
#11408=EDGE_LOOP('',(#5120,#5121,#5122,#5123));
#11409=EDGE_LOOP('',(#5124,#5125,#5126,#5127));
#11410=EDGE_LOOP('',(#5128,#5129,#5130,#5131));
#11411=EDGE_LOOP('',(#5132,#5133,#5134,#5135));
#11412=EDGE_LOOP('',(#5136,#5137,#5138,#5139));
#11413=EDGE_LOOP('',(#5140,#5141,#5142,#5143));
#11414=EDGE_LOOP('',(#5144,#5145,#5146,#5147));
#11415=EDGE_LOOP('',(#5148,#5149,#5150,#5151));
#11416=EDGE_LOOP('',(#5152,#5153,#5154,#5155));
#11417=EDGE_LOOP('',(#5156,#5157,#5158,#5159,#5160,#5161,#5162,#5163,#5164,
#5165,#5166,#5167,#5168,#5169,#5170,#5171,#5172,#5173,#5174,#5175,#5176));
#11418=EDGE_LOOP('',(#5177));
#11419=EDGE_LOOP('',(#5178));
#11420=EDGE_LOOP('',(#5179));
#12481=FACE_BOUND('',#11362,.T.);
#12482=FACE_BOUND('',#11363,.T.);
#12483=FACE_BOUND('',#11364,.T.);
#12484=FACE_BOUND('',#11365,.T.);
#12485=FACE_BOUND('',#11366,.T.);
#12486=FACE_BOUND('',#11367,.T.);
#12487=FACE_BOUND('',#11368,.T.);
#12488=FACE_BOUND('',#11369,.T.);
#12489=FACE_BOUND('',#11370,.T.);
#12490=FACE_BOUND('',#11371,.T.);
#12491=FACE_BOUND('',#11372,.T.);
#12492=FACE_BOUND('',#11373,.T.);
#12493=FACE_BOUND('',#11374,.T.);
#12494=FACE_BOUND('',#11375,.T.);
#12495=FACE_BOUND('',#11376,.T.);
#12496=FACE_BOUND('',#11377,.T.);
#12497=FACE_BOUND('',#11378,.T.);
#12498=FACE_BOUND('',#11379,.T.);
#12499=FACE_BOUND('',#11380,.T.);
#12500=FACE_BOUND('',#11381,.T.);
#12501=FACE_BOUND('',#11382,.T.);
#12502=FACE_BOUND('',#11383,.T.);
#12503=FACE_BOUND('',#11384,.T.);
#12504=FACE_BOUND('',#11385,.T.);
#12505=FACE_BOUND('',#11386,.T.);
#12506=FACE_BOUND('',#11387,.T.);
#12507=FACE_BOUND('',#11388,.T.);
#12508=FACE_BOUND('',#11389,.T.);
#12509=FACE_BOUND('',#11390,.T.);
#12510=FACE_BOUND('',#11391,.T.);
#12511=FACE_BOUND('',#11392,.T.);
#12512=FACE_BOUND('',#11393,.T.);
#12513=FACE_BOUND('',#11394,.T.);
#12514=FACE_BOUND('',#11395,.T.);
#12515=FACE_BOUND('',#11396,.T.);
#12516=FACE_BOUND('',#11397,.T.);
#12517=FACE_BOUND('',#11398,.T.);
#12518=FACE_BOUND('',#11399,.T.);
#12519=FACE_BOUND('',#11400,.T.);
#12520=FACE_BOUND('',#11401,.T.);
#12521=FACE_BOUND('',#11402,.T.);
#12522=FACE_BOUND('',#11403,.T.);
#12523=FACE_BOUND('',#11404,.T.);
#12524=FACE_BOUND('',#11405,.T.);
#12525=FACE_BOUND('',#11406,.T.);
#12526=FACE_BOUND('',#11407,.T.);
#12527=FACE_BOUND('',#11408,.T.);
#12528=FACE_BOUND('',#11409,.T.);
#12529=FACE_BOUND('',#11410,.T.);
#12530=FACE_BOUND('',#11411,.T.);
#12531=FACE_BOUND('',#11412,.T.);
#12532=FACE_BOUND('',#11413,.T.);
#12533=FACE_BOUND('',#11414,.T.);
#12534=FACE_BOUND('',#11415,.T.);
#12535=FACE_BOUND('',#11416,.T.);
#12536=FACE_BOUND('',#11417,.T.);
#12537=FACE_BOUND('',#11418,.T.);
#12538=FACE_BOUND('',#11419,.T.);
#12539=FACE_BOUND('',#11420,.T.);
#12693=(
BOUNDED_SURFACE()
B_SPLINE_SURFACE(1,2,((#39571,#39572,#39573,#39574,#39575,#39576,#39577,
#39578,#39579,#39580,#39581,#39582,#39583,#39584,#39585,#39586,#39587,#39588,
#39589,#39590,#39591,#39592,#39593,#39594,#39595,#39596,#39597,#39598,#39599,
#39600,#39601,#39602,#39603,#39604,#39605,#39606,#39607,#39608,#39609,#39610,
#39611,#39612,#39613,#39614,#39615,#39616,#39617,#39618,#39619,#39620,#39621,
#39622,#39623,#39624,#39625,#39626,#39627,#39628,#39629,#39630,#39631,#39632,
#39633,#39634,#39635,#39636,#39637,#39638,#39639,#39640,#39641,#39642,#39643,
#39644,#39645,#39646,#39647,#39648,#39649),(#39650,#39651,#39652,#39653,
#39654,#39655,#39656,#39657,#39658,#39659,#39660,#39661,#39662,#39663,#39664,
#39665,#39666,#39667,#39668,#39669,#39670,#39671,#39672,#39673,#39674,#39675,
#39676,#39677,#39678,#39679,#39680,#39681,#39682,#39683,#39684,#39685,#39686,
#39687,#39688,#39689,#39690,#39691,#39692,#39693,#39694,#39695,#39696,#39697,
#39698,#39699,#39700,#39701,#39702,#39703,#39704,#39705,#39706,#39707,#39708,
#39709,#39710,#39711,#39712,#39713,#39714,#39715,#39716,#39717,#39718,#39719,
#39720,#39721,#39722,#39723,#39724,#39725,#39726,#39727,#39728)),
 .RULED_SURF.,.F.,.F.,.F.)
B_SPLINE_SURFACE_WITH_KNOTS((2,2),(3,2,2,2,2,2,2,2,2,2,2,2,2,2,2,2,2,2,
2,2,2,2,2,2,2,2,2,2,2,2,2,2,2,2,2,2,2,2,2,3),(0.,1.),(0.,0.025,0.05,0.075,
0.1,0.125,0.15,0.175,0.2,0.225,0.25,0.275,0.3,0.325,0.35,0.375,0.4,0.425,
0.45,0.475,0.5,0.525,0.55,0.575,0.6,0.625,0.65,0.675,0.7,0.725,0.75,0.775,
0.8,0.825,0.85,0.875,0.9,0.925,0.95,0.9645502840563),.UNSPECIFIED.)
GEOMETRIC_REPRESENTATION_ITEM()
RATIONAL_B_SPLINE_SURFACE(((1.,0.951056516295154,1.,0.951056516295154,1.,
0.951056516295154,1.,0.951056516295154,1.,0.951056516295154,1.,0.951056516295154,
1.,0.951056516295154,1.,0.951056516295154,1.,0.951056516295154,1.,0.951056516295154,
1.,0.951056516295154,1.,0.951056516295154,1.,0.951056516295154,1.,0.951056516295154,
1.,0.951056516295154,1.,0.951056516295154,1.,0.951056516295154,1.,0.951056516295154,
1.,0.951056516295154,1.,0.951056516295154,1.,0.951056516295154,1.,0.951056516295154,
1.,0.951056516295154,1.,0.951056516295154,1.,0.951056516295154,1.,0.951056516295154,
1.,0.951056516295154,1.,0.951056516295154,1.,0.951056516295154,1.,0.951056516295154,
1.,0.951056516295154,1.,0.951056516295154,1.,0.951056516295154,1.,0.951056516295154,
1.,0.951056516295154,1.,0.951056516295154,1.,0.951056516295154,1.,0.951056516295154,
1.,0.971514336375583,0.976186632532565),(1.,0.951056516295154,1.,0.951056516295154,
1.,0.951056516295154,1.,0.951056516295154,1.,0.951056516295154,1.,0.951056516295154,
1.,0.951056516295154,1.,0.951056516295154,1.,0.951056516295154,1.,0.951056516295154,
1.,0.951056516295154,1.,0.951056516295154,1.,0.951056516295154,1.,0.951056516295154,
1.,0.951056516295154,1.,0.951056516295154,1.,0.951056516295154,1.,0.951056516295154,
1.,0.951056516295154,1.,0.951056516295154,1.,0.951056516295154,1.,0.951056516295154,
1.,0.951056516295154,1.,0.951056516295154,1.,0.951056516295154,1.,0.951056516295154,
1.,0.951056516295154,1.,0.951056516295154,1.,0.951056516295154,1.,0.951056516295154,
1.,0.951056516295154,1.,0.951056516295154,1.,0.951056516295154,1.,0.951056516295154,
1.,0.951056516295154,1.,0.951056516295154,1.,0.951056516295154,1.,0.951056516295154,
1.,0.971514336375583,0.976186632532565)))
REPRESENTATION_ITEM('')
SURFACE()
);
#12694=(
BOUNDED_SURFACE()
B_SPLINE_SURFACE(1,2,((#39925,#39926,#39927,#39928,#39929,#39930,#39931,
#39932,#39933,#39934,#39935,#39936,#39937,#39938,#39939,#39940,#39941,#39942,
#39943,#39944,#39945,#39946,#39947,#39948,#39949,#39950,#39951,#39952,#39953,
#39954,#39955,#39956,#39957,#39958,#39959,#39960,#39961,#39962,#39963,#39964,
#39965,#39966,#39967,#39968,#39969,#39970,#39971,#39972,#39973,#39974,#39975,
#39976,#39977,#39978,#39979,#39980,#39981,#39982,#39983,#39984,#39985,#39986,
#39987,#39988,#39989,#39990,#39991,#39992,#39993,#39994,#39995,#39996,#39997,
#39998,#39999,#40000,#40001,#40002,#40003,#40004,#40005),(#40006,#40007,
#40008,#40009,#40010,#40011,#40012,#40013,#40014,#40015,#40016,#40017,#40018,
#40019,#40020,#40021,#40022,#40023,#40024,#40025,#40026,#40027,#40028,#40029,
#40030,#40031,#40032,#40033,#40034,#40035,#40036,#40037,#40038,#40039,#40040,
#40041,#40042,#40043,#40044,#40045,#40046,#40047,#40048,#40049,#40050,#40051,
#40052,#40053,#40054,#40055,#40056,#40057,#40058,#40059,#40060,#40061,#40062,
#40063,#40064,#40065,#40066,#40067,#40068,#40069,#40070,#40071,#40072,#40073,
#40074,#40075,#40076,#40077,#40078,#40079,#40080,#40081,#40082,#40083,#40084,
#40085,#40086),(#40087,#40088,#40089,#40090,#40091,#40092,#40093,#40094,
#40095,#40096,#40097,#40098,#40099,#40100,#40101,#40102,#40103,#40104,#40105,
#40106,#40107,#40108,#40109,#40110,#40111,#40112,#40113,#40114,#40115,#40116,
#40117,#40118,#40119,#40120,#40121,#40122,#40123,#40124,#40125,#40126,#40127,
#40128,#40129,#40130,#40131,#40132,#40133,#40134,#40135,#40136,#40137,#40138,
#40139,#40140,#40141,#40142,#40143,#40144,#40145,#40146,#40147,#40148,#40149,
#40150,#40151,#40152,#40153,#40154,#40155,#40156,#40157,#40158,#40159,#40160,
#40161,#40162,#40163,#40164,#40165,#40166,#40167)),.RULED_SURF.,.F.,.F.,
 .F.)
B_SPLINE_SURFACE_WITH_KNOTS((2,1,2),(3,2,2,2,2,2,2,2,2,2,2,2,2,2,2,2,2,
2,2,2,2,2,2,2,2,2,2,2,2,2,2,2,2,2,2,2,2,2,2,2,3),(0.,1.,1.00600024802407),
(0.,0.025,0.05,0.075,0.1,0.125,0.15,0.175,0.2,0.225,0.25,0.275,0.3,0.325,
0.35,0.375,0.4,0.425,0.45,0.475,0.5,0.525,0.55,0.575,0.6,0.625,0.65,0.675,
0.7,0.725,0.75,0.775,0.8,0.825,0.85,0.875,0.9,0.925,0.95,0.964550250376854,
0.970337664573057),.PIECEWISE_BEZIER_KNOTS.)
GEOMETRIC_REPRESENTATION_ITEM()
RATIONAL_B_SPLINE_SURFACE(((1.,0.951056516295154,1.,0.951056516295154,1.,
0.951056516295154,1.,0.951056516295154,1.,0.951056516295154,1.,0.951056516295154,
1.,0.951056516295154,1.,0.951056516295154,1.,0.951056516295154,1.,0.951056516295154,
1.,0.951056516295154,1.,0.951056516295154,1.,0.951056516295154,1.,0.951056516295154,
1.,0.951056516295154,1.,0.951056516295154,1.,0.951056516295154,1.,0.951056516295154,
1.,0.951056516295154,1.,0.951056516295154,1.,0.951056516295154,1.,0.951056516295154,
1.,0.951056516295154,1.,0.951056516295154,1.,0.951056516295154,1.,0.951056516295154,
1.,0.951056516295154,1.,0.951056516295154,1.,0.951056516295154,1.,0.951056516295154,
1.,0.951056516295154,1.,0.951056516295154,1.,0.951056516295154,1.,0.951056516295154,
1.,0.951056516295154,1.,0.951056516295154,1.,0.951056516295154,1.,0.951056516295154,
1.,0.971514402311161,0.976186610902877,0.976186610902877,0.976186610902877),
(1.,0.951056516295154,1.,0.951056516295154,1.,0.951056516295154,1.,0.951056516295154,
1.,0.951056516295154,1.,0.951056516295154,1.,0.951056516295154,1.,0.951056516295154,
1.,0.951056516295154,1.,0.951056516295154,1.,0.951056516295154,1.,0.951056516295154,
1.,0.951056516295154,1.,0.951056516295154,1.,0.951056516295154,1.,0.951056516295154,
1.,0.951056516295154,1.,0.951056516295154,1.,0.951056516295154,1.,0.951056516295154,
1.,0.951056516295154,1.,0.951056516295154,1.,0.951056516295154,1.,0.951056516295154,
1.,0.951056516295154,1.,0.951056516295154,1.,0.951056516295154,1.,0.951056516295154,
1.,0.951056516295154,1.,0.951056516295154,1.,0.951056516295154,1.,0.951056516295154,
1.,0.951056516295154,1.,0.951056516295154,1.,0.951056516295154,1.,0.951056516295154,
1.,0.951056516295154,1.,0.951056516295154,1.,0.971514402311161,0.976186610902877,
0.976186610902877,0.976186610902877),(1.,0.951056516295154,1.,0.951056516295154,
1.,0.951056516295154,1.,0.951056516295154,1.,0.951056516295154,1.,0.951056516295154,
1.,0.951056516295154,1.,0.951056516295154,1.,0.951056516295154,1.,0.951056516295154,
1.,0.951056516295154,1.,0.951056516295154,1.,0.951056516295154,1.,0.951056516295154,
1.,0.951056516295154,1.,0.951056516295154,1.,0.951056516295154,1.,0.951056516295154,
1.,0.951056516295154,1.,0.951056516295154,1.,0.951056516295154,1.,0.951056516295154,
1.,0.951056516295154,1.,0.951056516295154,1.,0.951056516295154,1.,0.951056516295154,
1.,0.951056516295154,1.,0.951056516295154,1.,0.951056516295154,1.,0.951056516295154,
1.,0.951056516295154,1.,0.951056516295154,1.,0.951056516295154,1.,0.951056516295154,
1.,0.951056516295154,1.,0.951056516295154,1.,0.951056516295154,1.,0.951056516295154,
1.,0.971514402311161,0.976186610902877,0.976186610902877,0.976186610902877)))
REPRESENTATION_ITEM('')
SURFACE()
);
#13356=ADVANCED_FACE('',(#12481),#12693,.F.);
#13357=ADVANCED_FACE('',(#12482),#12694,.F.);
#13358=ADVANCED_FACE('',(#12483),#55,.F.);
#13359=ADVANCED_FACE('',(#12484),#1475,.F.);
#13360=ADVANCED_FACE('',(#12485),#1476,.T.);
#13361=ADVANCED_FACE('',(#12486),#1477,.F.);
#13362=ADVANCED_FACE('',(#12487),#1478,.F.);
#13363=ADVANCED_FACE('',(#12488),#1479,.F.);
#13364=ADVANCED_FACE('',(#12489),#1480,.F.);
#13365=ADVANCED_FACE('',(#12490),#1481,.F.);
#13366=ADVANCED_FACE('',(#12491),#1482,.F.);
#13367=ADVANCED_FACE('',(#12492),#1483,.F.);
#13368=ADVANCED_FACE('',(#12493),#1484,.F.);
#13369=ADVANCED_FACE('',(#12494),#1485,.F.);
#13370=ADVANCED_FACE('',(#12495),#1486,.F.);
#13371=ADVANCED_FACE('',(#12496),#1487,.F.);
#13372=ADVANCED_FACE('',(#12497),#1488,.F.);
#13373=ADVANCED_FACE('',(#12498),#1489,.F.);
#13374=ADVANCED_FACE('',(#12499),#1490,.F.);
#13375=ADVANCED_FACE('',(#12500),#1491,.F.);
#13376=ADVANCED_FACE('',(#12501),#1492,.F.);
#13377=ADVANCED_FACE('',(#12502),#1493,.F.);
#13378=ADVANCED_FACE('',(#12503),#1494,.F.);
#13379=ADVANCED_FACE('',(#12504),#1495,.F.);
#13380=ADVANCED_FACE('',(#12505),#1496,.F.);
#13381=ADVANCED_FACE('',(#12506),#1497,.F.);
#13382=ADVANCED_FACE('',(#12507),#1498,.F.);
#13383=ADVANCED_FACE('',(#12508),#1499,.F.);
#13384=ADVANCED_FACE('',(#12509),#1500,.F.);
#13385=ADVANCED_FACE('',(#12510),#1501,.F.);
#13386=ADVANCED_FACE('',(#12511),#1502,.F.);
#13387=ADVANCED_FACE('',(#12512),#1503,.F.);
#13388=ADVANCED_FACE('',(#12513),#1504,.F.);
#13389=ADVANCED_FACE('',(#12514),#1505,.F.);
#13390=ADVANCED_FACE('',(#12515),#1506,.F.);
#13391=ADVANCED_FACE('',(#12516),#1507,.F.);
#13392=ADVANCED_FACE('',(#12517),#1508,.F.);
#13393=ADVANCED_FACE('',(#12518),#1509,.F.);
#13394=ADVANCED_FACE('',(#12519,#12520),#1510,.T.);
#13395=ADVANCED_FACE('',(#12521,#12522),#1511,.F.);
#13396=ADVANCED_FACE('',(#12523),#1779,.T.);
#13397=ADVANCED_FACE('',(#12524,#12525),#1512,.F.);
#13398=ADVANCED_FACE('',(#12526),#1780,.T.);
#13399=ADVANCED_FACE('',(#12527),#1781,.T.);
#13400=ADVANCED_FACE('',(#12528),#1782,.T.);
#13401=ADVANCED_FACE('',(#12529),#1783,.T.);
#13402=ADVANCED_FACE('',(#12530),#1784,.T.);
#13403=ADVANCED_FACE('',(#12531),#1785,.T.);
#13404=ADVANCED_FACE('',(#12532),#1786,.T.);
#13405=ADVANCED_FACE('',(#12533),#1787,.T.);
#13406=ADVANCED_FACE('',(#12534),#1788,.T.);
#13407=ADVANCED_FACE('',(#12535),#1789,.T.);
#13408=ADVANCED_FACE('',(#12536,#12537),#1790,.T.);
#13409=ADVANCED_FACE('',(#12538,#12539),#1791,.F.);
#13524=CLOSED_SHELL('',(#13356,#13357,#13358,#13359,#13360,#13361,#13362,
#13363,#13364,#13365,#13366,#13367,#13368,#13369,#13370,#13371,#13372,#13373,
#13374,#13375,#13376,#13377,#13378,#13379,#13380,#13381,#13382,#13383,#13384,
#13385,#13386,#13387,#13388,#13389,#13390,#13391,#13392,#13393,#13394,#13395,
#13396,#13397,#13398,#13399,#13400,#13401,#13402,#13403,#13404,#13405,#13406,
#13407,#13408,#13409));
#13551=STYLED_ITEM('',(#13578),#13741);
#13578=PRESENTATION_STYLE_ASSIGNMENT((#13605));
#13605=SURFACE_STYLE_USAGE(.BOTH.,#13632);
#13632=SURFACE_SIDE_STYLE('',(#13659));
#13659=SURFACE_STYLE_FILL_AREA(#13686);
#13686=FILL_AREA_STYLE('',(#13713));
#13713=FILL_AREA_STYLE_COLOUR('',#60);
#13741=MANIFOLD_SOLID_BREP('refill_screw',#13524);
#13769=SHAPE_DEFINITION_REPRESENTATION(#45574,#13797);
#13797=SHAPE_REPRESENTATION('refill_screw',(#13802),#45487);
#13802=AXIS2_PLACEMENT_3D('',#19109,#15295,#15296);
#15049=AXIS2_PLACEMENT_3D('',#40821,#18437,#18438);
#15050=AXIS2_PLACEMENT_3D('',#40823,#18440,#18441);
#15051=AXIS2_PLACEMENT_3D('',#40825,#18443,#18444);
#15052=AXIS2_PLACEMENT_3D('',#40834,#18449,#18450);
#15053=AXIS2_PLACEMENT_3D('',#40840,#18454,#18455);
#15054=AXIS2_PLACEMENT_3D('',#40846,#18459,#18460);
#15055=AXIS2_PLACEMENT_3D('',#40855,#18465,#18466);
#15056=AXIS2_PLACEMENT_3D('',#40861,#18470,#18471);
#15057=AXIS2_PLACEMENT_3D('',#40867,#18475,#18476);
#15058=AXIS2_PLACEMENT_3D('',#40876,#18481,#18482);
#15059=AXIS2_PLACEMENT_3D('',#40882,#18486,#18487);
#15060=AXIS2_PLACEMENT_3D('',#40888,#18491,#18492);
#15061=AXIS2_PLACEMENT_3D('',#40897,#18497,#18498);
#15062=AXIS2_PLACEMENT_3D('',#40903,#18502,#18503);
#15063=AXIS2_PLACEMENT_3D('',#40909,#18507,#18508);
#15064=AXIS2_PLACEMENT_3D('',#40918,#18513,#18514);
#15065=AXIS2_PLACEMENT_3D('',#40924,#18518,#18519);
#15066=AXIS2_PLACEMENT_3D('',#40930,#18523,#18524);
#15067=AXIS2_PLACEMENT_3D('',#40939,#18529,#18530);
#15068=AXIS2_PLACEMENT_3D('',#40945,#18534,#18535);
#15069=AXIS2_PLACEMENT_3D('',#40951,#18539,#18540);
#15070=AXIS2_PLACEMENT_3D('',#40960,#18545,#18546);
#15071=AXIS2_PLACEMENT_3D('',#40966,#18550,#18551);
#15072=AXIS2_PLACEMENT_3D('',#40972,#18555,#18556);
#15073=AXIS2_PLACEMENT_3D('',#40981,#18561,#18562);
#15074=AXIS2_PLACEMENT_3D('',#40987,#18566,#18567);
#15075=AXIS2_PLACEMENT_3D('',#40993,#18571,#18572);
#15076=AXIS2_PLACEMENT_3D('',#41002,#18577,#18578);
#15077=AXIS2_PLACEMENT_3D('',#41008,#18582,#18583);
#15078=AXIS2_PLACEMENT_3D('',#41014,#18587,#18588);
#15079=AXIS2_PLACEMENT_3D('',#41023,#18593,#18594);
#15080=AXIS2_PLACEMENT_3D('',#41029,#18598,#18599);
#15081=AXIS2_PLACEMENT_3D('',#41035,#18603,#18604);
#15082=AXIS2_PLACEMENT_3D('',#41044,#18609,#18610);
#15083=AXIS2_PLACEMENT_3D('',#41050,#18614,#18615);
#15084=AXIS2_PLACEMENT_3D('',#41056,#18619,#18620);
#15085=AXIS2_PLACEMENT_3D('',#41057,#18621,#18622);
#15086=AXIS2_PLACEMENT_3D('',#41058,#18623,#18624);
#15087=AXIS2_PLACEMENT_3D('',#41059,#18625,#18626);
#15088=AXIS2_PLACEMENT_3D('',#41060,#18627,#18628);
#15089=AXIS2_PLACEMENT_3D('',#41061,#18629,#18630);
#15090=AXIS2_PLACEMENT_3D('',#41062,#18631,#18632);
#15091=AXIS2_PLACEMENT_3D('',#41063,#18633,#18634);
#15092=AXIS2_PLACEMENT_3D('',#41064,#18635,#18636);
#15093=AXIS2_PLACEMENT_3D('',#41065,#18637,#18638);
#15094=AXIS2_PLACEMENT_3D('',#41066,#18639,#18640);
#15095=AXIS2_PLACEMENT_3D('',#41067,#18641,#18642);
#15096=AXIS2_PLACEMENT_3D('',#41068,#18643,#18644);
#15097=AXIS2_PLACEMENT_3D('',#41070,#18645,#18646);
#15098=AXIS2_PLACEMENT_3D('',#41071,#18647,#18648);
#15099=AXIS2_PLACEMENT_3D('',#41072,#18649,#18650);
#15100=AXIS2_PLACEMENT_3D('',#41073,#18651,#18652);
#15101=AXIS2_PLACEMENT_3D('',#41074,#18653,#18654);
#15102=AXIS2_PLACEMENT_3D('',#41075,#18655,#18656);
#15103=AXIS2_PLACEMENT_3D('',#41076,#18657,#18658);
#15104=AXIS2_PLACEMENT_3D('',#41077,#18659,#18660);
#15105=AXIS2_PLACEMENT_3D('',#41078,#18661,#18662);
#15106=AXIS2_PLACEMENT_3D('',#41079,#18663,#18664);
#15107=AXIS2_PLACEMENT_3D('',#41080,#18665,#18666);
#15108=AXIS2_PLACEMENT_3D('',#41081,#18667,#18668);
#15109=AXIS2_PLACEMENT_3D('',#41082,#18669,#18670);
#15110=AXIS2_PLACEMENT_3D('',#41083,#18671,#18672);
#15111=AXIS2_PLACEMENT_3D('',#41084,#18673,#18674);
#15112=AXIS2_PLACEMENT_3D('',#41085,#18675,#18676);
#15113=AXIS2_PLACEMENT_3D('',#41087,#18677,#18678);
#15114=AXIS2_PLACEMENT_3D('',#41089,#18679,#18680);
#15115=AXIS2_PLACEMENT_3D('',#41090,#18681,#18682);
#15116=AXIS2_PLACEMENT_3D('',#41091,#18683,#18684);
#15117=AXIS2_PLACEMENT_3D('',#41092,#18685,#18686);
#15118=AXIS2_PLACEMENT_3D('',#41093,#18687,#18688);
#15119=AXIS2_PLACEMENT_3D('',#41094,#18689,#18690);
#15120=AXIS2_PLACEMENT_3D('',#41095,#18691,#18692);
#15121=AXIS2_PLACEMENT_3D('',#41096,#18693,#18694);
#15122=AXIS2_PLACEMENT_3D('',#41097,#18695,#18696);
#15123=AXIS2_PLACEMENT_3D('',#41098,#18697,#18698);
#15124=AXIS2_PLACEMENT_3D('',#41099,#18699,#18700);
#15125=AXIS2_PLACEMENT_3D('',#41100,#18701,#18702);
#15295=DIRECTION('',(0.,0.,1.));
#15296=DIRECTION('',(1.,0.,0.));
#18431=DIRECTION('',(0.86602540378444,-0.5,0.));
#18432=DIRECTION('',(-0.544728586009151,0.500000000000186,0.673253865628921));
#18433=DIRECTION('',(-0.86602540378444,-0.5,0.));
#18434=DIRECTION('',(0.544718486834211,0.499999449874283,-0.673262445281527));
#18435=DIRECTION('',(0.,-1.,0.));
#18436=DIRECTION('',(1.74897406310451E-5,0.99999999974693,1.41509078327272E-5));
#18437=DIRECTION('',(0.777406601108932,0.,0.628998391533919));
#18438=DIRECTION('',(0.628998391533919,0.,-0.777406601108932));
#18439=DIRECTION('',(0.,-1.,0.));
#18440=DIRECTION('',(0.,0.,1.));
#18441=DIRECTION('',(1.,0.,0.));
#18442=DIRECTION('',(0.,1.,0.));
#18443=DIRECTION('',(0.841253532831189,0.,0.540640817455586));
#18444=DIRECTION('',(0.540640817455586,0.,-0.841253532831189));
#18445=DIRECTION('',(0.,1.,0.));
#18446=DIRECTION('',(0.540640817455586,0.,-0.841253532831189));
#18447=DIRECTION('',(0.,1.,0.));
#18448=DIRECTION('',(-0.540640817455586,0.,0.841253532831189));
#18449=DIRECTION('',(0.540640817455586,0.,-0.841253532831189));
#18450=DIRECTION('',(-0.841253532831189,0.,-0.540640817455586));
#18451=DIRECTION('',(0.841253532831189,0.,0.540640817455586));
#18452=DIRECTION('',(-0.841253532831189,0.,-0.540640817455586));
#18453=DIRECTION('',(0.,1.,0.));
#18454=DIRECTION('',(-0.841253532831189,0.,-0.540640817455586));
#18455=DIRECTION('',(-0.540640817455586,0.,0.841253532831189));
#18456=DIRECTION('',(0.,-1.,0.));
#18457=DIRECTION('',(0.540640817455586,0.,-0.841253532831189));
#18458=DIRECTION('',(-0.540640817455586,0.,0.841253532831189));
#18459=DIRECTION('',(0.415415013001897,0.,0.909631995354513));
#18460=DIRECTION('',(0.909631995354513,0.,-0.415415013001897));
#18461=DIRECTION('',(0.,1.,0.));
#18462=DIRECTION('',(0.909631995354513,0.,-0.415415013001897));
#18463=DIRECTION('',(0.,1.,0.));
#18464=DIRECTION('',(-0.909631995354513,0.,0.415415013001897));
#18465=DIRECTION('',(0.909631995354513,0.,-0.415415013001897));
#18466=DIRECTION('',(-0.415415013001897,0.,-0.909631995354513));
#18467=DIRECTION('',(0.415415013001897,0.,0.909631995354513));
#18468=DIRECTION('',(-0.415415013001897,0.,-0.909631995354513));
#18469=DIRECTION('',(0.,1.,0.));
#18470=DIRECTION('',(-0.415415013001897,0.,-0.909631995354513));
#18471=DIRECTION('',(-0.909631995354513,0.,0.415415013001897));
#18472=DIRECTION('',(0.,-1.,0.));
#18473=DIRECTION('',(0.909631995354513,0.,-0.415415013001897));
#18474=DIRECTION('',(-0.909631995354513,0.,0.415415013001897));
#18475=DIRECTION('',(-0.142314838273275,0.,0.989821441880934));
#18476=DIRECTION('',(0.989821441880934,0.,0.142314838273275));
#18477=DIRECTION('',(0.,1.,0.));
#18478=DIRECTION('',(0.989821441880934,0.,0.142314838273275));
#18479=DIRECTION('',(0.,1.,0.));
#18480=DIRECTION('',(-0.989821441880934,0.,-0.142314838273275));
#18481=DIRECTION('',(0.989821441880934,0.,0.142314838273275));
#18482=DIRECTION('',(0.142314838273275,0.,-0.989821441880934));
#18483=DIRECTION('',(-0.142314838273275,0.,0.989821441880934));
#18484=DIRECTION('',(0.142314838273275,0.,-0.989821441880934));
#18485=DIRECTION('',(0.,1.,0.));
#18486=DIRECTION('',(0.142314838273275,0.,-0.989821441880934));
#18487=DIRECTION('',(-0.989821441880934,0.,-0.142314838273275));
#18488=DIRECTION('',(0.,-1.,0.));
#18489=DIRECTION('',(0.989821441880934,0.,0.142314838273275));
#18490=DIRECTION('',(-0.989821441880934,0.,-0.142314838273275));
#18491=DIRECTION('',(-0.654860733945278,0.,0.755749574354264));
#18492=DIRECTION('',(0.755749574354264,0.,0.654860733945278));
#18493=DIRECTION('',(0.,1.,0.));
#18494=DIRECTION('',(0.755749574354264,0.,0.654860733945278));
#18495=DIRECTION('',(0.,1.,0.));
#18496=DIRECTION('',(-0.755749574354264,0.,-0.654860733945278));
#18497=DIRECTION('',(0.755749574354264,0.,0.654860733945278));
#18498=DIRECTION('',(0.654860733945278,0.,-0.755749574354264));
#18499=DIRECTION('',(-0.654860733945278,0.,0.755749574354264));
#18500=DIRECTION('',(0.654860733945278,0.,-0.755749574354264));
#18501=DIRECTION('',(0.,1.,0.));
#18502=DIRECTION('',(0.654860733945278,0.,-0.755749574354264));
#18503=DIRECTION('',(-0.755749574354264,0.,-0.654860733945278));
#18504=DIRECTION('',(0.,-1.,0.));
#18505=DIRECTION('',(0.755749574354264,0.,0.654860733945278));
#18506=DIRECTION('',(-0.755749574354264,0.,-0.654860733945278));
#18507=DIRECTION('',(-0.959492973614495,0.,0.281732556841437));
#18508=DIRECTION('',(0.281732556841437,0.,0.959492973614495));
#18509=DIRECTION('',(0.,1.,0.));
#18510=DIRECTION('',(0.281732556841437,0.,0.959492973614495));
#18511=DIRECTION('',(0.,1.,0.));
#18512=DIRECTION('',(-0.281732556841437,0.,-0.959492973614495));
#18513=DIRECTION('',(0.281732556841437,0.,0.959492973614495));
#18514=DIRECTION('',(0.959492973614495,0.,-0.281732556841437));
#18515=DIRECTION('',(-0.959492973614495,0.,0.281732556841437));
#18516=DIRECTION('',(0.959492973614495,0.,-0.281732556841437));
#18517=DIRECTION('',(0.,1.,0.));
#18518=DIRECTION('',(0.959492973614495,0.,-0.281732556841437));
#18519=DIRECTION('',(-0.281732556841437,0.,-0.959492973614495));
#18520=DIRECTION('',(0.,-1.,0.));
#18521=DIRECTION('',(0.281732556841437,0.,0.959492973614495));
#18522=DIRECTION('',(-0.281732556841437,0.,-0.959492973614495));
#18523=DIRECTION('',(-0.959492973614499,0.,-0.281732556841423));
#18524=DIRECTION('',(-0.281732556841423,0.,0.959492973614499));
#18525=DIRECTION('',(0.,1.,0.));
#18526=DIRECTION('',(-0.281732556841423,0.,0.959492973614499));
#18527=DIRECTION('',(0.,1.,0.));
#18528=DIRECTION('',(0.281732556841423,0.,-0.959492973614499));
#18529=DIRECTION('',(-0.281732556841424,0.,0.959492973614499));
#18530=DIRECTION('',(0.959492973614499,0.,0.281732556841424));
#18531=DIRECTION('',(-0.959492973614499,0.,-0.281732556841424));
#18532=DIRECTION('',(0.959492973614499,0.,0.281732556841424));
#18533=DIRECTION('',(0.,1.,0.));
#18534=DIRECTION('',(0.959492973614499,0.,0.281732556841423));
#18535=DIRECTION('',(0.281732556841423,0.,-0.959492973614499));
#18536=DIRECTION('',(0.,-1.,0.));
#18537=DIRECTION('',(-0.281732556841423,0.,0.959492973614499));
#18538=DIRECTION('',(0.281732556841423,0.,-0.959492973614499));
#18539=DIRECTION('',(-0.654860733945289,0.,-0.755749574354255));
#18540=DIRECTION('',(-0.755749574354255,0.,0.654860733945289));
#18541=DIRECTION('',(0.,1.,0.));
#18542=DIRECTION('',(-0.755749574354255,0.,0.654860733945289));
#18543=DIRECTION('',(0.,1.,0.));
#18544=DIRECTION('',(0.755749574354255,0.,-0.654860733945289));
#18545=DIRECTION('',(-0.755749574354255,0.,0.654860733945289));
#18546=DIRECTION('',(0.654860733945289,0.,0.755749574354255));
#18547=DIRECTION('',(-0.654860733945289,0.,-0.755749574354255));
#18548=DIRECTION('',(0.654860733945289,0.,0.755749574354255));
#18549=DIRECTION('',(0.,1.,0.));
#18550=DIRECTION('',(0.654860733945289,0.,0.755749574354255));
#18551=DIRECTION('',(0.755749574354255,0.,-0.654860733945289));
#18552=DIRECTION('',(0.,-1.,0.));
#18553=DIRECTION('',(-0.755749574354255,0.,0.654860733945289));
#18554=DIRECTION('',(0.755749574354255,0.,-0.654860733945289));
#18555=DIRECTION('',(-0.142314838273289,0.,-0.989821441880932));
#18556=DIRECTION('',(-0.989821441880932,0.,0.142314838273289));
#18557=DIRECTION('',(0.,1.,0.));
#18558=DIRECTION('',(-0.989821441880932,0.,0.142314838273289));
#18559=DIRECTION('',(0.,1.,0.));
#18560=DIRECTION('',(0.989821441880932,0.,-0.142314838273289));
#18561=DIRECTION('',(-0.989821441880932,0.,0.142314838273289));
#18562=DIRECTION('',(0.142314838273289,0.,0.989821441880932));
#18563=DIRECTION('',(-0.142314838273289,0.,-0.989821441880932));
#18564=DIRECTION('',(0.142314838273289,0.,0.989821441880932));
#18565=DIRECTION('',(0.,1.,0.));
#18566=DIRECTION('',(0.142314838273289,0.,0.989821441880932));
#18567=DIRECTION('',(0.989821441880932,0.,-0.142314838273289));
#18568=DIRECTION('',(0.,-1.,0.));
#18569=DIRECTION('',(-0.989821441880932,0.,0.142314838273289));
#18570=DIRECTION('',(0.989821441880932,0.,-0.142314838273289));
#18571=DIRECTION('',(0.415415013001884,0.,-0.90963199535452));
#18572=DIRECTION('',(-0.90963199535452,0.,-0.415415013001884));
#18573=DIRECTION('',(0.,1.,0.));
#18574=DIRECTION('',(-0.909631995354519,0.,-0.415415013001884));
#18575=DIRECTION('',(0.,1.,0.));
#18576=DIRECTION('',(0.909631995354519,0.,0.415415013001884));
#18577=DIRECTION('',(-0.909631995354519,0.,-0.415415013001884));
#18578=DIRECTION('',(-0.415415013001884,0.,0.909631995354519));
#18579=DIRECTION('',(0.415415013001884,0.,-0.909631995354519));
#18580=DIRECTION('',(-0.415415013001884,0.,0.909631995354519));
#18581=DIRECTION('',(0.,1.,0.));
#18582=DIRECTION('',(-0.415415013001884,0.,0.90963199535452));
#18583=DIRECTION('',(0.90963199535452,0.,0.415415013001884));
#18584=DIRECTION('',(0.,-1.,0.));
#18585=DIRECTION('',(-0.90963199535452,0.,-0.415415013001884));
#18586=DIRECTION('',(0.90963199535452,0.,0.415415013001884));
#18587=DIRECTION('',(0.84125353283118,0.,-0.540640817455599));
#18588=DIRECTION('',(-0.540640817455599,0.,-0.84125353283118));
#18589=DIRECTION('',(0.,1.,0.));
#18590=DIRECTION('',(-0.540640817455599,0.,-0.84125353283118));
#18591=DIRECTION('',(0.,1.,0.));
#18592=DIRECTION('',(0.540640817455599,0.,0.84125353283118));
#18593=DIRECTION('',(-0.540640817455599,0.,-0.841253532831181));
#18594=DIRECTION('',(-0.841253532831181,0.,0.540640817455599));
#18595=DIRECTION('',(0.84125353283118,0.,-0.540640817455599));
#18596=DIRECTION('',(-0.84125353283118,0.,0.540640817455599));
#18597=DIRECTION('',(0.,1.,0.));
#18598=DIRECTION('',(-0.84125353283118,0.,0.540640817455599));
#18599=DIRECTION('',(0.540640817455599,0.,0.84125353283118));
#18600=DIRECTION('',(0.,-1.,0.));
#18601=DIRECTION('',(-0.540640817455599,0.,-0.84125353283118));
#18602=DIRECTION('',(0.540640817455599,0.,0.84125353283118));
#18603=DIRECTION('',(1.,0.,0.));
#18604=DIRECTION('',(0.,0.,-1.));
#18605=DIRECTION('',(0.,1.,0.));
#18606=DIRECTION('',(-1.14373924909521E-16,0.,-1.));
#18607=DIRECTION('',(0.,1.,0.));
#18608=DIRECTION('',(1.14373924909521E-16,0.,1.));
#18609=DIRECTION('',(0.,0.,-1.));
#18610=DIRECTION('',(-1.,0.,0.));
#18611=DIRECTION('',(1.,0.,0.));
#18612=DIRECTION('',(-1.,0.,0.));
#18613=DIRECTION('',(0.,1.,0.));
#18614=DIRECTION('',(-1.,0.,0.));
#18615=DIRECTION('',(0.,0.,1.));
#18616=DIRECTION('',(0.,-1.,0.));
#18617=DIRECTION('',(-1.71560887364281E-16,0.,-1.));
#18618=DIRECTION('',(1.71560887364281E-16,0.,1.));
#18619=DIRECTION('',(0.,1.,0.));
#18620=DIRECTION('',(0.,0.,1.));
#18621=DIRECTION('',(0.,1.,0.));
#18622=DIRECTION('',(0.,0.,1.));
#18623=DIRECTION('',(0.,1.,0.));
#18624=DIRECTION('',(0.,0.,1.));
#18625=DIRECTION('',(0.,1.,0.));
#18626=DIRECTION('',(0.,0.,1.));
#18627=DIRECTION('',(0.,1.,0.));
#18628=DIRECTION('',(0.,0.,1.));
#18629=DIRECTION('',(0.,1.,0.));
#18630=DIRECTION('',(0.,0.,1.));
#18631=DIRECTION('',(0.,1.,0.));
#18632=DIRECTION('',(0.,0.,1.));
#18633=DIRECTION('',(0.,1.,0.));
#18634=DIRECTION('',(0.,0.,1.));
#18635=DIRECTION('',(0.,1.,0.));
#18636=DIRECTION('',(0.,0.,1.));
#18637=DIRECTION('',(0.,1.,0.));
#18638=DIRECTION('',(0.,0.,1.));
#18639=DIRECTION('',(0.,1.,0.));
#18640=DIRECTION('',(0.,0.,1.));
#18641=DIRECTION('',(0.,1.,0.));
#18642=DIRECTION('',(0.,0.,1.));
#18643=DIRECTION('',(0.,1.,0.));
#18644=DIRECTION('',(0.,0.,1.));
#18645=DIRECTION('',(0.,1.,0.));
#18646=DIRECTION('',(0.,0.,1.));
#18647=DIRECTION('',(0.,1.,0.));
#18648=DIRECTION('',(0.,0.,1.));
#18649=DIRECTION('',(0.,1.,0.));
#18650=DIRECTION('',(0.,0.,1.));
#18651=DIRECTION('',(0.,1.,0.));
#18652=DIRECTION('',(0.,0.,1.));
#18653=DIRECTION('',(0.,1.,0.));
#18654=DIRECTION('',(0.,0.,1.));
#18655=DIRECTION('',(0.,1.,0.));
#18656=DIRECTION('',(0.,0.,1.));
#18657=DIRECTION('',(0.,1.,0.));
#18658=DIRECTION('',(0.,0.,1.));
#18659=DIRECTION('',(0.,1.,0.));
#18660=DIRECTION('',(0.,0.,1.));
#18661=DIRECTION('',(0.,1.,0.));
#18662=DIRECTION('',(0.,0.,1.));
#18663=DIRECTION('',(0.,1.,0.));
#18664=DIRECTION('',(0.,0.,1.));
#18665=DIRECTION('',(0.,1.,0.));
#18666=DIRECTION('',(0.,0.,1.));
#18667=DIRECTION('',(0.,1.,0.));
#18668=DIRECTION('',(0.,0.,1.));
#18669=DIRECTION('',(0.,1.,0.));
#18670=DIRECTION('',(0.,0.,1.));
#18671=DIRECTION('',(0.,1.,0.));
#18672=DIRECTION('',(0.,0.,1.));
#18673=DIRECTION('',(0.,1.,0.));
#18674=DIRECTION('',(0.,0.,1.));
#18675=DIRECTION('',(0.,1.,0.));
#18676=DIRECTION('',(0.,0.,1.));
#18677=DIRECTION('',(0.,1.,0.));
#18678=DIRECTION('',(0.,0.,1.));
#18679=DIRECTION('',(0.,1.,0.));
#18680=DIRECTION('',(0.,0.,1.));
#18681=DIRECTION('',(0.,1.,0.));
#18682=DIRECTION('',(0.,0.,1.));
#18683=DIRECTION('',(0.,1.,0.));
#18684=DIRECTION('',(0.,0.,1.));
#18685=DIRECTION('',(0.,1.,0.));
#18686=DIRECTION('',(0.,0.,1.));
#18687=DIRECTION('',(0.,1.,0.));
#18688=DIRECTION('',(0.,0.,1.));
#18689=DIRECTION('',(0.,1.,0.));
#18690=DIRECTION('',(0.,0.,1.));
#18691=DIRECTION('',(0.,1.,0.));
#18692=DIRECTION('',(0.,0.,1.));
#18693=DIRECTION('',(0.,1.,0.));
#18694=DIRECTION('',(0.,0.,1.));
#18695=DIRECTION('',(0.,1.,0.));
#18696=DIRECTION('',(0.,0.,1.));
#18697=DIRECTION('',(0.,1.,0.));
#18698=DIRECTION('',(0.,0.,1.));
#18699=DIRECTION('',(0.,-1.,0.));
#18700=DIRECTION('',(0.,0.,-1.));
#18701=DIRECTION('',(0.,1.,0.));
#18702=DIRECTION('',(0.,0.,1.));
#19109=CARTESIAN_POINT('',(0.,0.,0.));
#39571=CARTESIAN_POINT('',(-0.00598201094464286,0.0522062499024776,0.0466759019477942));
#39572=CARTESIAN_POINT('',(-0.00598201094464285,0.0521155356167633,0.0447322287687989));
#39573=CARTESIAN_POINT('',(-0.004839548514753,0.052024821331049,0.0431597641354809));
#39574=CARTESIAN_POINT('',(-0.00369708608486315,0.0519341070453347,0.041587299502163));
#39575=CARTESIAN_POINT('',(-0.00184854304243157,0.0518433927596204,0.0409866714583427));
#39576=CARTESIAN_POINT('',(-3.8514275599305E-19,0.0517526784739062,0.0403860434145223));
#39577=CARTESIAN_POINT('',(0.00184854304243157,0.0516619641881919,0.0409866714583427));
#39578=CARTESIAN_POINT('',(0.00369708608486315,0.0515712499024776,0.041587299502163));
#39579=CARTESIAN_POINT('',(0.004839548514753,0.0514805356167633,0.0431597641354809));
#39580=CARTESIAN_POINT('',(0.00598201094464285,0.0513898213310489,0.0447322287687989));
#39581=CARTESIAN_POINT('',(0.00598201094464286,0.0512991070453347,0.0466759019477942));
#39582=CARTESIAN_POINT('',(0.00598201094464286,0.0512083927596204,0.0486195751267895));
#39583=CARTESIAN_POINT('',(0.004839548514753,0.0511176784739062,0.0501920397601074));
#39584=CARTESIAN_POINT('',(0.00369708608486315,0.0510269641881918,0.0517645043934253));
#39585=CARTESIAN_POINT('',(0.00184854304243157,0.0509362499024776,0.0523651324372457));
#39586=CARTESIAN_POINT('',(1.15542826797915E-18,0.0508455356167633,0.052965760481066));
#39587=CARTESIAN_POINT('',(-0.00184854304243157,0.050754821331049,0.0523651324372457));
#39588=CARTESIAN_POINT('',(-0.00369708608486315,0.0506641070453347,0.0517645043934253));
#39589=CARTESIAN_POINT('',(-0.004839548514753,0.0505733927596204,0.0501920397601074));
#39590=CARTESIAN_POINT('',(-0.00598201094464285,0.0504826784739061,0.0486195751267895));
#39591=CARTESIAN_POINT('',(-0.00598201094464286,0.0503919641881919,0.0466759019477942));
#39592=CARTESIAN_POINT('',(-0.00598201094464285,0.0503012499024776,0.0447322287687989));
#39593=CARTESIAN_POINT('',(-0.004839548514753,0.0502105356167633,0.0431597641354809));
#39594=CARTESIAN_POINT('',(-0.00369708608486315,0.050119821331049,0.041587299502163));
#39595=CARTESIAN_POINT('',(-0.00184854304243157,0.0500291070453347,0.0409866714583427));
#39596=CARTESIAN_POINT('',(-3.8514275599305E-19,0.0499383927596204,0.0403860434145223));
#39597=CARTESIAN_POINT('',(0.00184854304243157,0.0498476784739062,0.0409866714583427));
#39598=CARTESIAN_POINT('',(0.00369708608486315,0.0497569641881919,0.041587299502163));
#39599=CARTESIAN_POINT('',(0.004839548514753,0.0496662499024776,0.0431597641354809));
#39600=CARTESIAN_POINT('',(0.00598201094464285,0.0495755356167633,0.0447322287687989));
#39601=CARTESIAN_POINT('',(0.00598201094464286,0.049484821331049,0.0466759019477942));
#39602=CARTESIAN_POINT('',(0.00598201094464286,0.0493941070453347,0.0486195751267895));
#39603=CARTESIAN_POINT('',(0.004839548514753,0.0493033927596204,0.0501920397601074));
#39604=CARTESIAN_POINT('',(0.00369708608486315,0.0492126784739062,0.0517645043934253));
#39605=CARTESIAN_POINT('',(0.00184854304243157,0.0491219641881919,0.0523651324372457));
#39606=CARTESIAN_POINT('',(1.15542826797915E-18,0.0490312499024775,0.052965760481066));
#39607=CARTESIAN_POINT('',(-0.00184854304243157,0.0489405356167633,0.0523651324372457));
#39608=CARTESIAN_POINT('',(-0.00369708608486315,0.048849821331049,0.0517645043934253));
#39609=CARTESIAN_POINT('',(-0.004839548514753,0.0487591070453347,0.0501920397601074));
#39610=CARTESIAN_POINT('',(-0.00598201094464285,0.0486683927596204,0.0486195751267895));
#39611=CARTESIAN_POINT('',(-0.00598201094464286,0.0485776784739062,0.0466759019477942));
#39612=CARTESIAN_POINT('',(-0.00598201094464285,0.0484869641881918,0.0447322287687989));
#39613=CARTESIAN_POINT('',(-0.004839548514753,0.0483962499024776,0.0431597641354809));
#39614=CARTESIAN_POINT('',(-0.00369708608486315,0.0483055356167633,0.041587299502163));
#39615=CARTESIAN_POINT('',(-0.00184854304243157,0.048214821331049,0.0409866714583427));
#39616=CARTESIAN_POINT('',(-3.8514275599305E-19,0.0481241070453347,0.0403860434145223));
#39617=CARTESIAN_POINT('',(0.00184854304243157,0.0480333927596204,0.0409866714583427));
#39618=CARTESIAN_POINT('',(0.00369708608486315,0.0479426784739061,0.041587299502163));
#39619=CARTESIAN_POINT('',(0.004839548514753,0.0478519641881919,0.0431597641354809));
#39620=CARTESIAN_POINT('',(0.00598201094464285,0.0477612499024776,0.0447322287687989));
#39621=CARTESIAN_POINT('',(0.00598201094464286,0.0476705356167633,0.0466759019477942));
#39622=CARTESIAN_POINT('',(0.00598201094464286,0.047579821331049,0.0486195751267895));
#39623=CARTESIAN_POINT('',(0.004839548514753,0.0474891070453347,0.0501920397601074));
#39624=CARTESIAN_POINT('',(0.00369708608486315,0.0473983927596204,0.0517645043934253));
#39625=CARTESIAN_POINT('',(0.00184854304243157,0.0473076784739062,0.0523651324372457));
#39626=CARTESIAN_POINT('',(1.15542826797915E-18,0.0472169641881919,0.052965760481066));
#39627=CARTESIAN_POINT('',(-0.00184854304243157,0.0471262499024776,0.0523651324372457));
#39628=CARTESIAN_POINT('',(-0.00369708608486315,0.0470355356167633,0.0517645043934253));
#39629=CARTESIAN_POINT('',(-0.004839548514753,0.046944821331049,0.0501920397601074));
#39630=CARTESIAN_POINT('',(-0.00598201094464285,0.0468541070453347,0.0486195751267895));
#39631=CARTESIAN_POINT('',(-0.00598201094464286,0.0467633927596204,0.0466759019477942));
#39632=CARTESIAN_POINT('',(-0.00598201094464285,0.0466726784739061,0.0447322287687989));
#39633=CARTESIAN_POINT('',(-0.004839548514753,0.0465819641881919,0.0431597641354809));
#39634=CARTESIAN_POINT('',(-0.00369708608486315,0.0464912499024775,0.041587299502163));
#39635=CARTESIAN_POINT('',(-0.00184854304243157,0.0464005356167633,0.0409866714583427));
#39636=CARTESIAN_POINT('',(-3.8514275599305E-19,0.046309821331049,0.0403860434145223));
#39637=CARTESIAN_POINT('',(0.00184854304243157,0.0462191070453347,0.0409866714583427));
#39638=CARTESIAN_POINT('',(0.00369708608486315,0.0461283927596204,0.041587299502163));
#39639=CARTESIAN_POINT('',(0.004839548514753,0.0460376784739062,0.0431597641354809));
#39640=CARTESIAN_POINT('',(0.00598201094464285,0.0459469641881919,0.0447322287687989));
#39641=CARTESIAN_POINT('',(0.00598201094464286,0.0458562499024776,0.0466759019477942));
#39642=CARTESIAN_POINT('',(0.00598201094464286,0.0457655356167633,0.0486195751267895));
#39643=CARTESIAN_POINT('',(0.004839548514753,0.045674821331049,0.0501920397601074));
#39644=CARTESIAN_POINT('',(0.00369708608486315,0.0455841070453347,0.0517645043934253));
#39645=CARTESIAN_POINT('',(0.00184854304243157,0.0454933927596204,0.0523651324372457));
#39646=CARTESIAN_POINT('',(1.15542826797915E-18,0.0454026784739061,0.052965760481066));
#39647=CARTESIAN_POINT('',(-0.00184854304243157,0.0453119641881919,0.0523651324372457));
#39648=CARTESIAN_POINT('',(-0.00290176072609688,0.0452602792191745,0.052022921267402));
#39649=CARTESIAN_POINT('',(-0.00376267526235443,0.0452060077307469,0.0513263567440365));
#39650=CARTESIAN_POINT('',(-0.005,0.0516392856192409,0.0466759019477942));
#39651=CARTESIAN_POINT('',(-0.005,0.0515485713335265,0.0450513034666296));
#39652=CARTESIAN_POINT('',(-0.00404508497187473,0.0514578570478123,0.0437369756863318));
#39653=CARTESIAN_POINT('',(-0.00309016994374947,0.0513671427620979,0.042422647906034));
#39654=CARTESIAN_POINT('',(-0.00154508497187473,0.0512764284763837,0.0419206193663185));
#39655=CARTESIAN_POINT('',(-3.21917461834437E-19,0.0511857141906694,0.0414185908266028));
#39656=CARTESIAN_POINT('',(0.00154508497187473,0.0510949999049552,0.0419206193663185));
#39657=CARTESIAN_POINT('',(0.00309016994374947,0.0510042856192408,0.042422647906034));
#39658=CARTESIAN_POINT('',(0.00404508497187473,0.0509135713335266,0.0437369756863318));
#39659=CARTESIAN_POINT('',(0.005,0.0508228570478123,0.0450513034666296));
#39660=CARTESIAN_POINT('',(0.005,0.050732142762098,0.0466759019477942));
#39661=CARTESIAN_POINT('',(0.005,0.0506414284763837,0.0483005004289586));
#39662=CARTESIAN_POINT('',(0.00404508497187473,0.0505507141906694,0.0496148282092566));
#39663=CARTESIAN_POINT('',(0.00309016994374947,0.0504599999049551,0.0509291559895544));
#39664=CARTESIAN_POINT('',(0.00154508497187473,0.0503692856192409,0.05143118452927));
#39665=CARTESIAN_POINT('',(9.65752385503311E-19,0.0502785713335266,0.0519332130689855));
#39666=CARTESIAN_POINT('',(-0.00154508497187473,0.0501878570478123,0.05143118452927));
#39667=CARTESIAN_POINT('',(-0.00309016994374947,0.050097142762098,0.0509291559895544));
#39668=CARTESIAN_POINT('',(-0.00404508497187473,0.0500064284763837,0.0496148282092566));
#39669=CARTESIAN_POINT('',(-0.005,0.0499157141906694,0.0483005004289586));
#39670=CARTESIAN_POINT('',(-0.005,0.0498249999049552,0.0466759019477942));
#39671=CARTESIAN_POINT('',(-0.005,0.0497342856192409,0.0450513034666296));
#39672=CARTESIAN_POINT('',(-0.00404508497187473,0.0496435713335266,0.0437369756863318));
#39673=CARTESIAN_POINT('',(-0.00309016994374947,0.0495528570478123,0.042422647906034));
#39674=CARTESIAN_POINT('',(-0.00154508497187473,0.049462142762098,0.0419206193663185));
#39675=CARTESIAN_POINT('',(-3.21917461834437E-19,0.0493714284763836,0.0414185908266028));
#39676=CARTESIAN_POINT('',(0.00154508497187473,0.0492807141906694,0.0419206193663185));
#39677=CARTESIAN_POINT('',(0.00309016994374947,0.0491899999049551,0.042422647906034));
#39678=CARTESIAN_POINT('',(0.00404508497187473,0.0490992856192409,0.0437369756863318));
#39679=CARTESIAN_POINT('',(0.005,0.0490085713335265,0.0450513034666296));
#39680=CARTESIAN_POINT('',(0.005,0.0489178570478123,0.0466759019477942));
#39681=CARTESIAN_POINT('',(0.005,0.048827142762098,0.0483005004289586));
#39682=CARTESIAN_POINT('',(0.00404508497187473,0.0487364284763837,0.0496148282092566));
#39683=CARTESIAN_POINT('',(0.00309016994374947,0.0486457141906694,0.0509291559895544));
#39684=CARTESIAN_POINT('',(0.00154508497187473,0.0485549999049552,0.05143118452927));
#39685=CARTESIAN_POINT('',(9.65752385503311E-19,0.0484642856192408,0.0519332130689855));
#39686=CARTESIAN_POINT('',(-0.00154508497187473,0.0483735713335266,0.05143118452927));
#39687=CARTESIAN_POINT('',(-0.00309016994374947,0.0482828570478123,0.0509291559895544));
#39688=CARTESIAN_POINT('',(-0.00404508497187473,0.048192142762098,0.0496148282092566));
#39689=CARTESIAN_POINT('',(-0.005,0.0481014284763837,0.0483005004289586));
#39690=CARTESIAN_POINT('',(-0.005,0.0480107141906694,0.0466759019477942));
#39691=CARTESIAN_POINT('',(-0.005,0.0479199999049551,0.0450513034666296));
#39692=CARTESIAN_POINT('',(-0.00404508497187473,0.0478292856192409,0.0437369756863318));
#39693=CARTESIAN_POINT('',(-0.00309016994374947,0.0477385713335266,0.042422647906034));
#39694=CARTESIAN_POINT('',(-0.00154508497187473,0.0476478570478123,0.0419206193663185));
#39695=CARTESIAN_POINT('',(-3.21917461834437E-19,0.047557142762098,0.0414185908266028));
#39696=CARTESIAN_POINT('',(0.00154508497187473,0.0474664284763837,0.0419206193663185));
#39697=CARTESIAN_POINT('',(0.00309016994374947,0.0473757141906694,0.042422647906034));
#39698=CARTESIAN_POINT('',(0.00404508497187473,0.0472849999049552,0.0437369756863318));
#39699=CARTESIAN_POINT('',(0.005,0.0471942856192409,0.0450513034666296));
#39700=CARTESIAN_POINT('',(0.005,0.0471035713335266,0.0466759019477942));
#39701=CARTESIAN_POINT('',(0.005,0.0470128570478123,0.0483005004289586));
#39702=CARTESIAN_POINT('',(0.00404508497187473,0.046922142762098,0.0496148282092566));
#39703=CARTESIAN_POINT('',(0.00309016994374947,0.0468314284763837,0.0509291559895544));
#39704=CARTESIAN_POINT('',(0.00154508497187473,0.0467407141906694,0.05143118452927));
#39705=CARTESIAN_POINT('',(9.65752385503311E-19,0.0466499999049551,0.0519332130689855));
#39706=CARTESIAN_POINT('',(-0.00154508497187473,0.0465592856192409,0.05143118452927));
#39707=CARTESIAN_POINT('',(-0.00309016994374947,0.0464685713335266,0.0509291559895544));
#39708=CARTESIAN_POINT('',(-0.00404508497187473,0.0463778570478123,0.0496148282092566));
#39709=CARTESIAN_POINT('',(-0.005,0.046287142762098,0.0483005004289586));
#39710=CARTESIAN_POINT('',(-0.005,0.0461964284763837,0.0466759019477942));
#39711=CARTESIAN_POINT('',(-0.005,0.0461057141906694,0.0450513034666296));
#39712=CARTESIAN_POINT('',(-0.00404508497187473,0.0460149999049552,0.0437369756863318));
#39713=CARTESIAN_POINT('',(-0.00309016994374947,0.0459242856192409,0.042422647906034));
#39714=CARTESIAN_POINT('',(-0.00154508497187473,0.0458335713335266,0.0419206193663185));
#39715=CARTESIAN_POINT('',(-3.21917461834437E-19,0.0457428570478123,0.0414185908266028));
#39716=CARTESIAN_POINT('',(0.00154508497187473,0.045652142762098,0.0419206193663185));
#39717=CARTESIAN_POINT('',(0.00309016994374947,0.0455614284763837,0.042422647906034));
#39718=CARTESIAN_POINT('',(0.00404508497187473,0.0454707141906694,0.0437369756863318));
#39719=CARTESIAN_POINT('',(0.005,0.0453799999049551,0.0450513034666296));
#39720=CARTESIAN_POINT('',(0.005,0.0452892856192409,0.0466759019477942));
#39721=CARTESIAN_POINT('',(0.005,0.0451985713335266,0.0483005004289586));
#39722=CARTESIAN_POINT('',(0.00404508497187473,0.0451078570478123,0.0496148282092566));
#39723=CARTESIAN_POINT('',(0.00309016994374947,0.045017142762098,0.0509291559895544));
#39724=CARTESIAN_POINT('',(0.00154508497187473,0.0449264284763837,0.05143118452927));
#39725=CARTESIAN_POINT('',(9.65752385503311E-19,0.0448357141906694,0.0519332130689855));
#39726=CARTESIAN_POINT('',(-0.00154508497187473,0.0447449999049551,0.05143118452927));
#39727=CARTESIAN_POINT('',(-0.00242540573140837,0.0446933149359378,0.0511451509754948));
#39728=CARTESIAN_POINT('',(-0.0031449919576995,0.0446390434475102,0.0505629349533147));
#39729=CARTESIAN_POINT('',(-0.00549100547232143,0.0519227677608592,0.0466759019477942));
#39730=CARTESIAN_POINT('',(-0.00598201094464286,0.0522062499024776,0.0466759019477942));
#39731=CARTESIAN_POINT('',(-0.005,0.0516392856192409,0.0466759019477942));
#39732=CARTESIAN_POINT('',(-0.00598201094464286,0.0522062499024776,0.0466759019477942));
#39733=CARTESIAN_POINT('',(-0.00598201094464285,0.0521155356167633,0.0447322287687989));
#39734=CARTESIAN_POINT('',(-0.004839548514753,0.052024821331049,0.0431597641354809));
#39735=CARTESIAN_POINT('',(-0.00369708608486315,0.0519341070453347,0.041587299502163));
#39736=CARTESIAN_POINT('',(-0.00184854304243157,0.0518433927596204,0.0409866714583427));
#39737=CARTESIAN_POINT('',(-3.8514275599305E-19,0.0517526784739062,0.0403860434145223));
#39738=CARTESIAN_POINT('',(0.00184854304243157,0.0516619641881919,0.0409866714583427));
#39739=CARTESIAN_POINT('',(0.00369708608486315,0.0515712499024776,0.041587299502163));
#39740=CARTESIAN_POINT('',(0.004839548514753,0.0514805356167633,0.0431597641354809));
#39741=CARTESIAN_POINT('',(0.00598201094464285,0.0513898213310489,0.0447322287687989));
#39742=CARTESIAN_POINT('',(0.00598201094464286,0.0512991070453347,0.0466759019477942));
#39743=CARTESIAN_POINT('',(0.00598201094464286,0.0512083927596204,0.0486195751267895));
#39744=CARTESIAN_POINT('',(0.004839548514753,0.0511176784739062,0.0501920397601074));
#39745=CARTESIAN_POINT('',(0.00369708608486315,0.0510269641881918,0.0517645043934253));
#39746=CARTESIAN_POINT('',(0.00184854304243157,0.0509362499024776,0.0523651324372457));
#39747=CARTESIAN_POINT('',(1.15542826797915E-18,0.0508455356167633,0.052965760481066));
#39748=CARTESIAN_POINT('',(-0.00184854304243157,0.050754821331049,0.0523651324372457));
#39749=CARTESIAN_POINT('',(-0.00369708608486315,0.0506641070453347,0.0517645043934253));
#39750=CARTESIAN_POINT('',(-0.004839548514753,0.0505733927596204,0.0501920397601074));
#39751=CARTESIAN_POINT('',(-0.00598201094464285,0.0504826784739061,0.0486195751267895));
#39752=CARTESIAN_POINT('',(-0.00598201094464286,0.0503919641881919,0.0466759019477942));
#39753=CARTESIAN_POINT('',(-0.00598201094464285,0.0503012499024776,0.0447322287687989));
#39754=CARTESIAN_POINT('',(-0.004839548514753,0.0502105356167633,0.0431597641354809));
#39755=CARTESIAN_POINT('',(-0.00369708608486315,0.050119821331049,0.041587299502163));
#39756=CARTESIAN_POINT('',(-0.00184854304243157,0.0500291070453347,0.0409866714583427));
#39757=CARTESIAN_POINT('',(-3.8514275599305E-19,0.0499383927596204,0.0403860434145223));
#39758=CARTESIAN_POINT('',(0.00184854304243157,0.0498476784739062,0.0409866714583427));
#39759=CARTESIAN_POINT('',(0.00369708608486315,0.0497569641881919,0.041587299502163));
#39760=CARTESIAN_POINT('',(0.004839548514753,0.0496662499024776,0.0431597641354809));
#39761=CARTESIAN_POINT('',(0.00598201094464285,0.0495755356167633,0.0447322287687989));
#39762=CARTESIAN_POINT('',(0.00598201094464286,0.049484821331049,0.0466759019477942));
#39763=CARTESIAN_POINT('',(0.00598201094464286,0.0493941070453347,0.0486195751267895));
#39764=CARTESIAN_POINT('',(0.004839548514753,0.0493033927596204,0.0501920397601074));
#39765=CARTESIAN_POINT('',(0.00369708608486315,0.0492126784739062,0.0517645043934253));
#39766=CARTESIAN_POINT('',(0.00184854304243157,0.0491219641881919,0.0523651324372457));
#39767=CARTESIAN_POINT('',(1.15542826797915E-18,0.0490312499024775,0.052965760481066));
#39768=CARTESIAN_POINT('',(-0.00184854304243157,0.0489405356167633,0.0523651324372457));
#39769=CARTESIAN_POINT('',(-0.00369708608486315,0.0488498213310489,0.0517645043934253));
#39770=CARTESIAN_POINT('',(-0.004839548514753,0.0487591070453347,0.0501920397601074));
#39771=CARTESIAN_POINT('',(-0.00598201094464285,0.0486683927596204,0.0486195751267895));
#39772=CARTESIAN_POINT('',(-0.00598201094464286,0.0485776784739062,0.0466759019477942));
#39773=CARTESIAN_POINT('',(-0.00598201094464285,0.0484869641881918,0.0447322287687989));
#39774=CARTESIAN_POINT('',(-0.004839548514753,0.0483962499024776,0.0431597641354809));
#39775=CARTESIAN_POINT('',(-0.00369708608486315,0.0483055356167633,0.041587299502163));
#39776=CARTESIAN_POINT('',(-0.00184854304243157,0.048214821331049,0.0409866714583427));
#39777=CARTESIAN_POINT('',(-3.8514275599305E-19,0.0481241070453347,0.0403860434145223));
#39778=CARTESIAN_POINT('',(0.00184854304243157,0.0480333927596204,0.0409866714583427));
#39779=CARTESIAN_POINT('',(0.00369708608486315,0.0479426784739061,0.041587299502163));
#39780=CARTESIAN_POINT('',(0.004839548514753,0.0478519641881919,0.0431597641354809));
#39781=CARTESIAN_POINT('',(0.00598201094464285,0.0477612499024776,0.0447322287687989));
#39782=CARTESIAN_POINT('',(0.00598201094464286,0.0476705356167633,0.0466759019477942));
#39783=CARTESIAN_POINT('',(0.00598201094464286,0.047579821331049,0.0486195751267895));
#39784=CARTESIAN_POINT('',(0.004839548514753,0.0474891070453347,0.0501920397601074));
#39785=CARTESIAN_POINT('',(0.00369708608486315,0.0473983927596204,0.0517645043934253));
#39786=CARTESIAN_POINT('',(0.00184854304243157,0.0473076784739062,0.0523651324372457));
#39787=CARTESIAN_POINT('',(1.15542826797915E-18,0.0472169641881919,0.052965760481066));
#39788=CARTESIAN_POINT('',(-0.00184854304243157,0.0471262499024776,0.0523651324372457));
#39789=CARTESIAN_POINT('',(-0.00369708608486315,0.0470355356167633,0.0517645043934253));
#39790=CARTESIAN_POINT('',(-0.004839548514753,0.046944821331049,0.0501920397601074));
#39791=CARTESIAN_POINT('',(-0.00598201094464285,0.0468541070453347,0.0486195751267895));
#39792=CARTESIAN_POINT('',(-0.00598201094464286,0.0467633927596204,0.0466759019477942));
#39793=CARTESIAN_POINT('',(-0.00598201094464285,0.0466726784739061,0.0447322287687989));
#39794=CARTESIAN_POINT('',(-0.004839548514753,0.0465819641881919,0.0431597641354809));
#39795=CARTESIAN_POINT('',(-0.00369708608486315,0.0464912499024775,0.041587299502163));
#39796=CARTESIAN_POINT('',(-0.00184854304243157,0.0464005356167633,0.0409866714583427));
#39797=CARTESIAN_POINT('',(-3.8514275599305E-19,0.046309821331049,0.0403860434145223));
#39798=CARTESIAN_POINT('',(0.00184854304243157,0.0462191070453347,0.0409866714583427));
#39799=CARTESIAN_POINT('',(0.00369708608486315,0.0461283927596204,0.041587299502163));
#39800=CARTESIAN_POINT('',(0.004839548514753,0.0460376784739062,0.0431597641354809));
#39801=CARTESIAN_POINT('',(0.00598201094464285,0.0459469641881919,0.0447322287687989));
#39802=CARTESIAN_POINT('',(0.00598201094464286,0.0458562499024776,0.0466759019477942));
#39803=CARTESIAN_POINT('',(0.00598201094464286,0.0457655356167633,0.0486195751267895));
#39804=CARTESIAN_POINT('',(0.004839548514753,0.045674821331049,0.0501920397601074));
#39805=CARTESIAN_POINT('',(0.00369708608486315,0.0455841070453347,0.0517645043934253));
#39806=CARTESIAN_POINT('',(0.00184854304243157,0.0454933927596204,0.0523651324372457));
#39807=CARTESIAN_POINT('',(1.15542826797915E-18,0.0454026784739061,0.052965760481066));
#39808=CARTESIAN_POINT('',(-0.00184854304243157,0.0453119641881919,0.0523651324372457));
#39809=CARTESIAN_POINT('',(-0.00290176072609409,0.0452602792191746,0.052022921267403));
#39810=CARTESIAN_POINT('',(-0.00376267526235003,0.0452060077307472,0.05132635674404));
#39811=CARTESIAN_POINT('',(-0.00376267526235003,0.0452060077307471,0.0513263567440401));
#39812=CARTESIAN_POINT('',(-0.00345383361002476,0.0449225255891286,0.0509446458486774));
#39813=CARTESIAN_POINT('',(-0.0031449919576995,0.0446390434475102,0.0505629349533147));
#39814=CARTESIAN_POINT('',(8.89120054436383E-19,0.0448357141906694,0.0516759019477941));
#39815=CARTESIAN_POINT('',(-0.00079192220162268,0.0447892192352662,0.0516759019477941));
#39816=CARTESIAN_POINT('',(-0.00154508497187473,0.0447449999049551,0.05143118452927));
#39817=CARTESIAN_POINT('',(-0.00242540573140837,0.0446933149359378,0.0511451509754948));
#39818=CARTESIAN_POINT('',(-0.0031449919576995,0.0446390434475102,0.0505629349533147));
#39819=CARTESIAN_POINT('',(8.89120054436383E-19,0.0448357141906695,0.0516759019477942));
#39820=CARTESIAN_POINT('',(-2.22280013609096E-19,0.0457428570478123,0.0416759019477942));
#39821=CARTESIAN_POINT('',(0.000791922201622681,0.0456963620924091,0.0416759019477942));
#39822=CARTESIAN_POINT('',(0.00154508497187473,0.045652142762098,0.0419206193663185));
#39823=CARTESIAN_POINT('',(0.00309016994374947,0.0455614284763837,0.042422647906034));
#39824=CARTESIAN_POINT('',(0.00404508497187473,0.0454707141906694,0.0437369756863318));
#39825=CARTESIAN_POINT('',(0.005,0.0453799999049551,0.0450513034666297));
#39826=CARTESIAN_POINT('',(0.005,0.0452892856192409,0.0466759019477942));
#39827=CARTESIAN_POINT('',(0.005,0.0451985713335266,0.0483005004289586));
#39828=CARTESIAN_POINT('',(0.00404508497187473,0.0451078570478123,0.0496148282092566));
#39829=CARTESIAN_POINT('',(0.00309016994374947,0.045017142762098,0.0509291559895544));
#39830=CARTESIAN_POINT('',(0.00154508497187473,0.0449264284763837,0.05143118452927));
#39831=CARTESIAN_POINT('',(0.000791922201622682,0.0448822091460727,0.0516759019477941));
#39832=CARTESIAN_POINT('',(8.89120054436383E-19,0.0448357141906694,0.0516759019477941));
#39833=CARTESIAN_POINT('',(-2.22280013609096E-19,0.0457428570478123,0.0416759019477942));
#39834=CARTESIAN_POINT('',(8.89120054436383E-19,0.0466499999049551,0.0516759019477941));
#39835=CARTESIAN_POINT('',(-0.00079192220162268,0.046603504949552,0.0516759019477941));
#39836=CARTESIAN_POINT('',(-0.00154508497187473,0.0465592856192409,0.05143118452927));
#39837=CARTESIAN_POINT('',(-0.00309016994374947,0.0464685713335266,0.0509291559895544));
#39838=CARTESIAN_POINT('',(-0.00404508497187473,0.0463778570478123,0.0496148282092566));
#39839=CARTESIAN_POINT('',(-0.005,0.046287142762098,0.0483005004289586));
#39840=CARTESIAN_POINT('',(-0.005,0.0461964284763837,0.0466759019477942));
#39841=CARTESIAN_POINT('',(-0.005,0.0461057141906694,0.0450513034666297));
#39842=CARTESIAN_POINT('',(-0.00404508497187473,0.0460149999049552,0.0437369756863318));
#39843=CARTESIAN_POINT('',(-0.00309016994374947,0.0459242856192409,0.042422647906034));
#39844=CARTESIAN_POINT('',(-0.00154508497187473,0.0458335713335266,0.0419206193663185));
#39845=CARTESIAN_POINT('',(-0.000791922201622681,0.0457893520032155,0.0416759019477942));
#39846=CARTESIAN_POINT('',(-2.22280013609096E-19,0.0457428570478123,0.0416759019477942));
#39847=CARTESIAN_POINT('',(8.89120054436383E-19,0.0466499999049552,0.0516759019477942));
#39848=CARTESIAN_POINT('',(-2.22280013609096E-19,0.047557142762098,0.0416759019477942));
#39849=CARTESIAN_POINT('',(0.000791922201622681,0.0475106478066948,0.0416759019477942));
#39850=CARTESIAN_POINT('',(0.00154508497187473,0.0474664284763837,0.0419206193663185));
#39851=CARTESIAN_POINT('',(0.00309016994374947,0.0473757141906694,0.042422647906034));
#39852=CARTESIAN_POINT('',(0.00404508497187473,0.0472849999049552,0.0437369756863318));
#39853=CARTESIAN_POINT('',(0.005,0.0471942856192409,0.0450513034666297));
#39854=CARTESIAN_POINT('',(0.005,0.0471035713335266,0.0466759019477942));
#39855=CARTESIAN_POINT('',(0.005,0.0470128570478123,0.0483005004289586));
#39856=CARTESIAN_POINT('',(0.00404508497187473,0.046922142762098,0.0496148282092566));
#39857=CARTESIAN_POINT('',(0.00309016994374947,0.0468314284763837,0.0509291559895544));
#39858=CARTESIAN_POINT('',(0.00154508497187473,0.0467407141906694,0.05143118452927));
#39859=CARTESIAN_POINT('',(0.000791922201622682,0.0466964948603584,0.0516759019477941));
#39860=CARTESIAN_POINT('',(8.89120054436383E-19,0.0466499999049551,0.0516759019477941));
#39861=CARTESIAN_POINT('',(-2.22280013609096E-19,0.047557142762098,0.0416759019477942));
#39862=CARTESIAN_POINT('',(8.89120054436383E-19,0.0484642856192409,0.0516759019477941));
#39863=CARTESIAN_POINT('',(-0.00079192220162268,0.0484177906638377,0.0516759019477941));
#39864=CARTESIAN_POINT('',(-0.00154508497187473,0.0483735713335266,0.05143118452927));
#39865=CARTESIAN_POINT('',(-0.00309016994374947,0.0482828570478123,0.0509291559895544));
#39866=CARTESIAN_POINT('',(-0.00404508497187473,0.048192142762098,0.0496148282092566));
#39867=CARTESIAN_POINT('',(-0.005,0.0481014284763837,0.0483005004289586));
#39868=CARTESIAN_POINT('',(-0.005,0.0480107141906694,0.0466759019477942));
#39869=CARTESIAN_POINT('',(-0.005,0.0479199999049551,0.0450513034666297));
#39870=CARTESIAN_POINT('',(-0.00404508497187473,0.0478292856192409,0.0437369756863318));
#39871=CARTESIAN_POINT('',(-0.00309016994374947,0.0477385713335266,0.042422647906034));
#39872=CARTESIAN_POINT('',(-0.00154508497187473,0.0476478570478123,0.0419206193663185));
#39873=CARTESIAN_POINT('',(-0.000791922201622681,0.0476036377175013,0.0416759019477942));
#39874=CARTESIAN_POINT('',(-2.22280013609096E-19,0.047557142762098,0.0416759019477942));
#39875=CARTESIAN_POINT('',(8.89120054436383E-19,0.0484642856192409,0.0516759019477942));
#39876=CARTESIAN_POINT('',(-2.22280013609096E-19,0.0493714284763837,0.0416759019477942));
#39877=CARTESIAN_POINT('',(0.000791922201622681,0.0493249335209805,0.0416759019477942));
#39878=CARTESIAN_POINT('',(0.00154508497187473,0.0492807141906694,0.0419206193663185));
#39879=CARTESIAN_POINT('',(0.00309016994374947,0.0491899999049551,0.042422647906034));
#39880=CARTESIAN_POINT('',(0.00404508497187473,0.0490992856192409,0.0437369756863318));
#39881=CARTESIAN_POINT('',(0.005,0.0490085713335265,0.0450513034666297));
#39882=CARTESIAN_POINT('',(0.005,0.0489178570478123,0.0466759019477942));
#39883=CARTESIAN_POINT('',(0.005,0.048827142762098,0.0483005004289586));
#39884=CARTESIAN_POINT('',(0.00404508497187473,0.0487364284763837,0.0496148282092566));
#39885=CARTESIAN_POINT('',(0.00309016994374947,0.0486457141906694,0.0509291559895544));
#39886=CARTESIAN_POINT('',(0.00154508497187473,0.0485549999049552,0.05143118452927));
#39887=CARTESIAN_POINT('',(0.000791922201622682,0.0485107805746441,0.0516759019477941));
#39888=CARTESIAN_POINT('',(8.89120054436383E-19,0.0484642856192409,0.0516759019477941));
#39889=CARTESIAN_POINT('',(-2.22280013609096E-19,0.0493714284763837,0.0416759019477942));
#39890=CARTESIAN_POINT('',(8.89120054436383E-19,0.0502785713335266,0.0516759019477941));
#39891=CARTESIAN_POINT('',(-0.00079192220162268,0.0502320763781233,0.0516759019477941));
#39892=CARTESIAN_POINT('',(-0.00154508497187473,0.0501878570478123,0.05143118452927));
#39893=CARTESIAN_POINT('',(-0.00309016994374947,0.050097142762098,0.0509291559895544));
#39894=CARTESIAN_POINT('',(-0.00404508497187473,0.0500064284763837,0.0496148282092566));
#39895=CARTESIAN_POINT('',(-0.005,0.0499157141906694,0.0483005004289586));
#39896=CARTESIAN_POINT('',(-0.005,0.0498249999049552,0.0466759019477942));
#39897=CARTESIAN_POINT('',(-0.005,0.0497342856192409,0.0450513034666297));
#39898=CARTESIAN_POINT('',(-0.00404508497187473,0.0496435713335266,0.0437369756863318));
#39899=CARTESIAN_POINT('',(-0.00309016994374947,0.0495528570478123,0.042422647906034));
#39900=CARTESIAN_POINT('',(-0.00154508497187473,0.049462142762098,0.0419206193663185));
#39901=CARTESIAN_POINT('',(-0.000791922201622681,0.0494179234317869,0.0416759019477942));
#39902=CARTESIAN_POINT('',(-2.22280013609096E-19,0.0493714284763837,0.0416759019477942));
#39903=CARTESIAN_POINT('',(8.89120054436383E-19,0.0502785713335266,0.0516759019477942));
#39904=CARTESIAN_POINT('',(-2.22280013609096E-19,0.0511857141906695,0.0416759019477942));
#39905=CARTESIAN_POINT('',(0.000791922201622681,0.0511392192352662,0.0416759019477942));
#39906=CARTESIAN_POINT('',(0.00154508497187473,0.0510949999049552,0.0419206193663185));
#39907=CARTESIAN_POINT('',(0.00309016994374947,0.0510042856192408,0.042422647906034));
#39908=CARTESIAN_POINT('',(0.00404508497187473,0.0509135713335266,0.0437369756863318));
#39909=CARTESIAN_POINT('',(0.005,0.0508228570478122,0.0450513034666297));
#39910=CARTESIAN_POINT('',(0.005,0.050732142762098,0.0466759019477942));
#39911=CARTESIAN_POINT('',(0.005,0.0506414284763837,0.0483005004289586));
#39912=CARTESIAN_POINT('',(0.00404508497187473,0.0505507141906694,0.0496148282092566));
#39913=CARTESIAN_POINT('',(0.00309016994374947,0.0504599999049551,0.0509291559895544));
#39914=CARTESIAN_POINT('',(0.00154508497187473,0.0503692856192409,0.05143118452927));
#39915=CARTESIAN_POINT('',(0.000791922201622682,0.0503250662889298,0.0516759019477941));
#39916=CARTESIAN_POINT('',(8.89120054436383E-19,0.0502785713335266,0.0516759019477941));
#39917=CARTESIAN_POINT('',(-2.22280013609096E-19,0.0511857141906694,0.0416759019477942));
#39918=CARTESIAN_POINT('',(-0.005,0.0516392856192409,0.0466759019477942));
#39919=CARTESIAN_POINT('',(-0.005,0.0515485713335265,0.0450513034666297));
#39920=CARTESIAN_POINT('',(-0.00404508497187473,0.0514578570478123,0.0437369756863318));
#39921=CARTESIAN_POINT('',(-0.00309016994374947,0.0513671427620979,0.042422647906034));
#39922=CARTESIAN_POINT('',(-0.00154508497187473,0.0512764284763837,0.0419206193663185));
#39923=CARTESIAN_POINT('',(-0.000791922201622681,0.0512322091460726,0.0416759019477942));
#39924=CARTESIAN_POINT('',(-2.22280013609096E-19,0.0511857141906695,0.0416759019477942));
#39925=CARTESIAN_POINT('',(-0.005,0.0529999999,0.0466759019477942));
#39926=CARTESIAN_POINT('',(-0.005,0.0529092856142857,0.0450513034666296));
#39927=CARTESIAN_POINT('',(-0.00404508497187473,0.0528185713285714,0.0437369756863318));
#39928=CARTESIAN_POINT('',(-0.00309016994374947,0.0527278570428571,0.042422647906034));
#39929=CARTESIAN_POINT('',(-0.00154508497187473,0.0526371427571429,0.0419206193663185));
#39930=CARTESIAN_POINT('',(-3.21917461834437E-19,0.0525464284714285,0.0414185908266028));
#39931=CARTESIAN_POINT('',(0.00154508497187473,0.0524557141857143,0.0419206193663185));
#39932=CARTESIAN_POINT('',(0.00309016994374947,0.0523649999,0.042422647906034));
#39933=CARTESIAN_POINT('',(0.00404508497187473,0.0522742856142857,0.0437369756863318));
#39934=CARTESIAN_POINT('',(0.005,0.0521835713285714,0.0450513034666296));
#39935=CARTESIAN_POINT('',(0.005,0.0520928570428571,0.0466759019477942));
#39936=CARTESIAN_POINT('',(0.005,0.0520021427571428,0.0483005004289586));
#39937=CARTESIAN_POINT('',(0.00404508497187473,0.0519114284714286,0.0496148282092566));
#39938=CARTESIAN_POINT('',(0.00309016994374947,0.0518207141857143,0.0509291559895544));
#39939=CARTESIAN_POINT('',(0.00154508497187473,0.0517299999,0.05143118452927));
#39940=CARTESIAN_POINT('',(9.65752385503311E-19,0.0516392856142857,0.0519332130689855));
#39941=CARTESIAN_POINT('',(-0.00154508497187473,0.0515485713285714,0.05143118452927));
#39942=CARTESIAN_POINT('',(-0.00309016994374947,0.0514578570428571,0.0509291559895544));
#39943=CARTESIAN_POINT('',(-0.00404508497187473,0.0513671427571429,0.0496148282092566));
#39944=CARTESIAN_POINT('',(-0.005,0.0512764284714286,0.0483005004289586));
#39945=CARTESIAN_POINT('',(-0.005,0.0511857141857143,0.0466759019477942));
#39946=CARTESIAN_POINT('',(-0.005,0.0510949999,0.0450513034666296));
#39947=CARTESIAN_POINT('',(-0.00404508497187473,0.0510042856142857,0.0437369756863318));
#39948=CARTESIAN_POINT('',(-0.00309016994374947,0.0509135713285715,0.042422647906034));
#39949=CARTESIAN_POINT('',(-0.00154508497187473,0.0508228570428571,0.0419206193663185));
#39950=CARTESIAN_POINT('',(-3.21917461834437E-19,0.0507321427571428,0.0414185908266028));
#39951=CARTESIAN_POINT('',(0.00154508497187473,0.0506414284714286,0.0419206193663185));
#39952=CARTESIAN_POINT('',(0.00309016994374947,0.0505507141857142,0.042422647906034));
#39953=CARTESIAN_POINT('',(0.00404508497187473,0.0504599999,0.0437369756863318));
#39954=CARTESIAN_POINT('',(0.005,0.0503692856142857,0.0450513034666296));
#39955=CARTESIAN_POINT('',(0.005,0.0502785713285714,0.0466759019477942));
#39956=CARTESIAN_POINT('',(0.005,0.0501878570428571,0.0483005004289586));
#39957=CARTESIAN_POINT('',(0.00404508497187473,0.0500971427571429,0.0496148282092566));
#39958=CARTESIAN_POINT('',(0.00309016994374947,0.0500064284714285,0.0509291559895544));
#39959=CARTESIAN_POINT('',(0.00154508497187473,0.0499157141857143,0.05143118452927));
#39960=CARTESIAN_POINT('',(9.65752385503311E-19,0.0498249999,0.0519332130689855));
#39961=CARTESIAN_POINT('',(-0.00154508497187473,0.0497342856142857,0.05143118452927));
#39962=CARTESIAN_POINT('',(-0.00309016994374947,0.0496435713285714,0.0509291559895544));
#39963=CARTESIAN_POINT('',(-0.00404508497187473,0.0495528570428571,0.0496148282092566));
#39964=CARTESIAN_POINT('',(-0.005,0.0494621427571428,0.0483005004289586));
#39965=CARTESIAN_POINT('',(-0.005,0.0493714284714286,0.0466759019477942));
#39966=CARTESIAN_POINT('',(-0.005,0.0492807141857143,0.0450513034666296));
#39967=CARTESIAN_POINT('',(-0.00404508497187473,0.0491899999,0.0437369756863318));
#39968=CARTESIAN_POINT('',(-0.00309016994374947,0.0490992856142857,0.042422647906034));
#39969=CARTESIAN_POINT('',(-0.00154508497187473,0.0490085713285714,0.0419206193663185));
#39970=CARTESIAN_POINT('',(-3.21917461834437E-19,0.0489178570428572,0.0414185908266028));
#39971=CARTESIAN_POINT('',(0.00154508497187473,0.0488271427571429,0.0419206193663185));
#39972=CARTESIAN_POINT('',(0.00309016994374947,0.0487364284714286,0.042422647906034));
#39973=CARTESIAN_POINT('',(0.00404508497187473,0.0486457141857143,0.0437369756863318));
#39974=CARTESIAN_POINT('',(0.005,0.0485549999,0.0450513034666296));
#39975=CARTESIAN_POINT('',(0.005,0.0484642856142857,0.0466759019477942));
#39976=CARTESIAN_POINT('',(0.005,0.0483735713285714,0.0483005004289586));
#39977=CARTESIAN_POINT('',(0.00404508497187473,0.0482828570428571,0.0496148282092566));
#39978=CARTESIAN_POINT('',(0.00309016994374947,0.0481921427571428,0.0509291559895544));
#39979=CARTESIAN_POINT('',(0.00154508497187473,0.0481014284714286,0.05143118452927));
#39980=CARTESIAN_POINT('',(9.65752385503311E-19,0.0480107141857142,0.0519332130689855));
#39981=CARTESIAN_POINT('',(-0.00154508497187473,0.0479199999,0.05143118452927));
#39982=CARTESIAN_POINT('',(-0.00309016994374947,0.0478292856142857,0.0509291559895544));
#39983=CARTESIAN_POINT('',(-0.00404508497187473,0.0477385713285714,0.0496148282092566));
#39984=CARTESIAN_POINT('',(-0.005,0.0476478570428571,0.0483005004289586));
#39985=CARTESIAN_POINT('',(-0.005,0.0475571427571429,0.0466759019477942));
#39986=CARTESIAN_POINT('',(-0.005,0.0474664284714285,0.0450513034666296));
#39987=CARTESIAN_POINT('',(-0.00404508497187473,0.0473757141857143,0.0437369756863318));
#39988=CARTESIAN_POINT('',(-0.00309016994374947,0.0472849999,0.042422647906034));
#39989=CARTESIAN_POINT('',(-0.00154508497187473,0.0471942856142857,0.0419206193663185));
#39990=CARTESIAN_POINT('',(-3.21917461834437E-19,0.0471035713285714,0.0414185908266028));
#39991=CARTESIAN_POINT('',(0.00154508497187473,0.0470128570428571,0.0419206193663185));
#39992=CARTESIAN_POINT('',(0.00309016994374947,0.0469221427571428,0.042422647906034));
#39993=CARTESIAN_POINT('',(0.00404508497187473,0.0468314284714286,0.0437369756863318));
#39994=CARTESIAN_POINT('',(0.005,0.0467407141857143,0.0450513034666296));
#39995=CARTESIAN_POINT('',(0.005,0.0466499999,0.0466759019477942));
#39996=CARTESIAN_POINT('',(0.005,0.0465592856142857,0.0483005004289586));
#39997=CARTESIAN_POINT('',(0.00404508497187473,0.0464685713285714,0.0496148282092566));
#39998=CARTESIAN_POINT('',(0.00309016994374947,0.0463778570428571,0.0509291559895544));
#39999=CARTESIAN_POINT('',(0.00154508497187473,0.0462871427571429,0.05143118452927));
#40000=CARTESIAN_POINT('',(9.65752385503311E-19,0.0461964284714286,0.0519332130689855));
#40001=CARTESIAN_POINT('',(-0.00154508497187473,0.0461057141857143,0.05143118452927));
#40002=CARTESIAN_POINT('',(-0.00242540363398948,0.0460540293398396,0.0511451516569875));
#40003=CARTESIAN_POINT('',(-0.00314498864239956,0.0459997579783105,0.050562937635716));
#40004=CARTESIAN_POINT('',(-0.00342983626690057,0.0459782746674725,0.0503324682971777));
#40005=CARTESIAN_POINT('',(-0.00371468389140158,0.0459567913566346,0.0501019989586393));
#40006=CARTESIAN_POINT('',(-0.00598201094464286,0.0524330356167633,0.0466759019477942));
#40007=CARTESIAN_POINT('',(-0.00598201094464285,0.052342321331049,0.0447322287687989));
#40008=CARTESIAN_POINT('',(-0.004839548514753,0.0522516070453347,0.0431597641354809));
#40009=CARTESIAN_POINT('',(-0.00369708608486315,0.0521608927596204,0.041587299502163));
#40010=CARTESIAN_POINT('',(-0.00184854304243157,0.0520701784739062,0.0409866714583427));
#40011=CARTESIAN_POINT('',(-3.8514275599305E-19,0.0519794641881918,0.0403860434145223));
#40012=CARTESIAN_POINT('',(0.00184854304243157,0.0518887499024776,0.0409866714583427));
#40013=CARTESIAN_POINT('',(0.00369708608486315,0.0517980356167633,0.041587299502163));
#40014=CARTESIAN_POINT('',(0.004839548514753,0.051707321331049,0.0431597641354809));
#40015=CARTESIAN_POINT('',(0.00598201094464285,0.0516166070453347,0.0447322287687989));
#40016=CARTESIAN_POINT('',(0.00598201094464286,0.0515258927596204,0.0466759019477942));
#40017=CARTESIAN_POINT('',(0.00598201094464286,0.0514351784739062,0.0486195751267895));
#40018=CARTESIAN_POINT('',(0.004839548514753,0.0513444641881919,0.0501920397601074));
#40019=CARTESIAN_POINT('',(0.00369708608486315,0.0512537499024776,0.0517645043934253));
#40020=CARTESIAN_POINT('',(0.00184854304243157,0.0511630356167633,0.0523651324372457));
#40021=CARTESIAN_POINT('',(1.15542826797915E-18,0.051072321331049,0.052965760481066));
#40022=CARTESIAN_POINT('',(-0.00184854304243157,0.0509816070453347,0.0523651324372457));
#40023=CARTESIAN_POINT('',(-0.00369708608486315,0.0508908927596205,0.0517645043934253));
#40024=CARTESIAN_POINT('',(-0.004839548514753,0.0508001784739061,0.0501920397601074));
#40025=CARTESIAN_POINT('',(-0.00598201094464285,0.0507094641881918,0.0486195751267895));
#40026=CARTESIAN_POINT('',(-0.00598201094464286,0.0506187499024776,0.0466759019477942));
#40027=CARTESIAN_POINT('',(-0.00598201094464285,0.0505280356167632,0.0447322287687989));
#40028=CARTESIAN_POINT('',(-0.004839548514753,0.050437321331049,0.0431597641354809));
#40029=CARTESIAN_POINT('',(-0.00369708608486315,0.0503466070453347,0.041587299502163));
#40030=CARTESIAN_POINT('',(-0.00184854304243157,0.0502558927596204,0.0409866714583427));
#40031=CARTESIAN_POINT('',(-3.8514275599305E-19,0.0501651784739061,0.0403860434145223));
#40032=CARTESIAN_POINT('',(0.00184854304243157,0.0500744641881919,0.0409866714583427));
#40033=CARTESIAN_POINT('',(0.00369708608486315,0.0499837499024775,0.041587299502163));
#40034=CARTESIAN_POINT('',(0.004839548514753,0.0498930356167633,0.0431597641354809));
#40035=CARTESIAN_POINT('',(0.00598201094464285,0.049802321331049,0.0447322287687989));
#40036=CARTESIAN_POINT('',(0.00598201094464286,0.0497116070453347,0.0466759019477942));
#40037=CARTESIAN_POINT('',(0.00598201094464286,0.0496208927596204,0.0486195751267895));
#40038=CARTESIAN_POINT('',(0.004839548514753,0.0495301784739061,0.0501920397601074));
#40039=CARTESIAN_POINT('',(0.00369708608486315,0.0494394641881919,0.0517645043934253));
#40040=CARTESIAN_POINT('',(0.00184854304243157,0.0493487499024776,0.0523651324372457));
#40041=CARTESIAN_POINT('',(1.15542826797915E-18,0.0492580356167633,0.052965760481066));
#40042=CARTESIAN_POINT('',(-0.00184854304243157,0.049167321331049,0.0523651324372457));
#40043=CARTESIAN_POINT('',(-0.00369708608486315,0.0490766070453347,0.0517645043934253));
#40044=CARTESIAN_POINT('',(-0.004839548514753,0.0489858927596204,0.0501920397601074));
#40045=CARTESIAN_POINT('',(-0.00598201094464285,0.0488951784739062,0.0486195751267895));
#40046=CARTESIAN_POINT('',(-0.00598201094464286,0.0488044641881919,0.0466759019477942));
#40047=CARTESIAN_POINT('',(-0.00598201094464285,0.0487137499024776,0.0447322287687989));
#40048=CARTESIAN_POINT('',(-0.004839548514753,0.0486230356167633,0.0431597641354809));
#40049=CARTESIAN_POINT('',(-0.00369708608486315,0.0485323213310489,0.041587299502163));
#40050=CARTESIAN_POINT('',(-0.00184854304243157,0.0484416070453347,0.0409866714583427));
#40051=CARTESIAN_POINT('',(-3.8514275599305E-19,0.0483508927596204,0.0403860434145223));
#40052=CARTESIAN_POINT('',(0.00184854304243157,0.0482601784739061,0.0409866714583427));
#40053=CARTESIAN_POINT('',(0.00369708608486315,0.0481694641881918,0.041587299502163));
#40054=CARTESIAN_POINT('',(0.004839548514753,0.0480787499024776,0.0431597641354809));
#40055=CARTESIAN_POINT('',(0.00598201094464285,0.0479880356167633,0.0447322287687989));
#40056=CARTESIAN_POINT('',(0.00598201094464286,0.047897321331049,0.0466759019477942));
#40057=CARTESIAN_POINT('',(0.00598201094464286,0.0478066070453347,0.0486195751267895));
#40058=CARTESIAN_POINT('',(0.004839548514753,0.0477158927596204,0.0501920397601074));
#40059=CARTESIAN_POINT('',(0.00369708608486315,0.0476251784739061,0.0517645043934253));
#40060=CARTESIAN_POINT('',(0.00184854304243157,0.0475344641881919,0.0523651324372457));
#40061=CARTESIAN_POINT('',(1.15542826797915E-18,0.0474437499024775,0.052965760481066));
#40062=CARTESIAN_POINT('',(-0.00184854304243157,0.0473530356167633,0.0523651324372457));
#40063=CARTESIAN_POINT('',(-0.00369708608486315,0.047262321331049,0.0517645043934253));
#40064=CARTESIAN_POINT('',(-0.004839548514753,0.0471716070453347,0.0501920397601074));
#40065=CARTESIAN_POINT('',(-0.00598201094464285,0.0470808927596204,0.0486195751267895));
#40066=CARTESIAN_POINT('',(-0.00598201094464286,0.0469901784739061,0.0466759019477942));
#40067=CARTESIAN_POINT('',(-0.00598201094464285,0.0468994641881918,0.0447322287687989));
#40068=CARTESIAN_POINT('',(-0.004839548514753,0.0468087499024776,0.0431597641354809));
#40069=CARTESIAN_POINT('',(-0.00369708608486315,0.0467180356167633,0.041587299502163));
#40070=CARTESIAN_POINT('',(-0.00184854304243157,0.046627321331049,0.0409866714583427));
#40071=CARTESIAN_POINT('',(-3.8514275599305E-19,0.0465366070453347,0.0403860434145223));
#40072=CARTESIAN_POINT('',(0.00184854304243157,0.0464458927596204,0.0409866714583427));
#40073=CARTESIAN_POINT('',(0.00369708608486315,0.0463551784739062,0.041587299502163));
#40074=CARTESIAN_POINT('',(0.004839548514753,0.0462644641881919,0.0431597641354809));
#40075=CARTESIAN_POINT('',(0.00598201094464285,0.0461737499024775,0.0447322287687989));
#40076=CARTESIAN_POINT('',(0.00598201094464286,0.0460830356167633,0.0466759019477942));
#40077=CARTESIAN_POINT('',(0.00598201094464286,0.045992321331049,0.0486195751267895));
#40078=CARTESIAN_POINT('',(0.004839548514753,0.0459016070453347,0.0501920397601074));
#40079=CARTESIAN_POINT('',(0.00369708608486315,0.0458108927596204,0.0517645043934253));
#40080=CARTESIAN_POINT('',(0.00184854304243157,0.0457201784739062,0.0523651324372457));
#40081=CARTESIAN_POINT('',(1.15542826797915E-18,0.0456294641881918,0.052965760481066));
#40082=CARTESIAN_POINT('',(-0.00184854304243157,0.0455387499024776,0.0523651324372457));
#40083=CARTESIAN_POINT('',(-0.00290175821674032,0.0454870650566028,0.0520229220827414));
#40084=CARTESIAN_POINT('',(-0.00376267129592233,0.0454327936950738,0.0513263599532673));
#40085=CARTESIAN_POINT('',(-0.00410346361738644,0.0454113103842358,0.0510506259321592));
#40086=CARTESIAN_POINT('',(-0.00444425593885055,0.0453898270733979,0.050774891911051));
#40087=CARTESIAN_POINT('',(-0.00598790325387306,0.0524296336904431,0.0466759019477942));
#40088=CARTESIAN_POINT('',(-0.00598790325387306,0.0523389194047288,0.0447303142414737));
#40089=CARTESIAN_POINT('',(-0.00484431549305635,0.0522482051190145,0.0431563007230135));
#40090=CARTESIAN_POINT('',(-0.00370072773223964,0.0521574908333002,0.0415822872045532));
#40091=CARTESIAN_POINT('',(-0.00185036386611982,0.052066776547586,0.0409810675392532));
#40092=CARTESIAN_POINT('',(-3.85522123439397E-19,0.0519760622618717,0.0403798478739532));
#40093=CARTESIAN_POINT('',(0.00185036386611982,0.0518853479761574,0.0409810675392532));
#40094=CARTESIAN_POINT('',(0.00370072773223964,0.0517946336904431,0.0415822872045532));
#40095=CARTESIAN_POINT('',(0.00484431549305635,0.0517039194047288,0.0431563007230135));
#40096=CARTESIAN_POINT('',(0.00598790325387306,0.0516132051190145,0.0447303142414737));
#40097=CARTESIAN_POINT('',(0.00598790325387306,0.0515224908333002,0.0466759019477942));
#40098=CARTESIAN_POINT('',(0.00598790325387306,0.051431776547586,0.0486214896541146));
#40099=CARTESIAN_POINT('',(0.00484431549305635,0.0513410622618717,0.0501955031725749));
#40100=CARTESIAN_POINT('',(0.00370072773223964,0.0512503479761574,0.0517695166910351));
#40101=CARTESIAN_POINT('',(0.00185036386611982,0.0511596336904431,0.0523707363563351));
#40102=CARTESIAN_POINT('',(1.15656637031819E-18,0.0510689194047287,0.0529719560216351));
#40103=CARTESIAN_POINT('',(-0.00185036386611982,0.0509782051190145,0.0523707363563351));
#40104=CARTESIAN_POINT('',(-0.00370072773223964,0.0508874908333002,0.0517695166910351));
#40105=CARTESIAN_POINT('',(-0.00484431549305635,0.0507967765475859,0.0501955031725749));
#40106=CARTESIAN_POINT('',(-0.00598790325387306,0.0507060622618716,0.0486214896541146));
#40107=CARTESIAN_POINT('',(-0.00598790325387306,0.0506153479761574,0.0466759019477942));
#40108=CARTESIAN_POINT('',(-0.00598790325387306,0.050524633690443,0.0447303142414737));
#40109=CARTESIAN_POINT('',(-0.00484431549305635,0.0504339194047288,0.0431563007230135));
#40110=CARTESIAN_POINT('',(-0.00370072773223964,0.0503432051190145,0.0415822872045532));
#40111=CARTESIAN_POINT('',(-0.00185036386611982,0.0502524908333002,0.0409810675392532));
#40112=CARTESIAN_POINT('',(-3.85522123439397E-19,0.0501617765475859,0.0403798478739532));
#40113=CARTESIAN_POINT('',(0.00185036386611982,0.0500710622618717,0.0409810675392532));
#40114=CARTESIAN_POINT('',(0.00370072773223964,0.0499803479761574,0.0415822872045532));
#40115=CARTESIAN_POINT('',(0.00484431549305635,0.0498896336904431,0.0431563007230135));
#40116=CARTESIAN_POINT('',(0.00598790325387306,0.0497989194047288,0.0447303142414737));
#40117=CARTESIAN_POINT('',(0.00598790325387306,0.0497082051190145,0.0466759019477942));
#40118=CARTESIAN_POINT('',(0.00598790325387306,0.0496174908333002,0.0486214896541146));
#40119=CARTESIAN_POINT('',(0.00484431549305635,0.0495267765475859,0.0501955031725749));
#40120=CARTESIAN_POINT('',(0.00370072773223964,0.0494360622618717,0.0517695166910351));
#40121=CARTESIAN_POINT('',(0.00185036386611982,0.0493453479761574,0.0523707363563351));
#40122=CARTESIAN_POINT('',(1.15656637031819E-18,0.0492546336904431,0.0529719560216351));
#40123=CARTESIAN_POINT('',(-0.00185036386611982,0.0491639194047288,0.0523707363563351));
#40124=CARTESIAN_POINT('',(-0.00370072773223964,0.0490732051190145,0.0517695166910351));
#40125=CARTESIAN_POINT('',(-0.00484431549305635,0.0489824908333002,0.0501955031725749));
#40126=CARTESIAN_POINT('',(-0.00598790325387306,0.048891776547586,0.0486214896541146));
#40127=CARTESIAN_POINT('',(-0.00598790325387306,0.0488010622618717,0.0466759019477942));
#40128=CARTESIAN_POINT('',(-0.00598790325387306,0.0487103479761573,0.0447303142414737));
#40129=CARTESIAN_POINT('',(-0.00484431549305635,0.0486196336904431,0.0431563007230135));
#40130=CARTESIAN_POINT('',(-0.00370072773223964,0.0485289194047288,0.0415822872045532));
#40131=CARTESIAN_POINT('',(-0.00185036386611982,0.0484382051190145,0.0409810675392532));
#40132=CARTESIAN_POINT('',(-3.85522123439397E-19,0.0483474908333002,0.0403798478739532));
#40133=CARTESIAN_POINT('',(0.00185036386611982,0.0482567765475859,0.0409810675392532));
#40134=CARTESIAN_POINT('',(0.00370072773223964,0.0481660622618716,0.0415822872045532));
#40135=CARTESIAN_POINT('',(0.00484431549305635,0.0480753479761574,0.0431563007230135));
#40136=CARTESIAN_POINT('',(0.00598790325387306,0.0479846336904431,0.0447303142414737));
#40137=CARTESIAN_POINT('',(0.00598790325387306,0.0478939194047288,0.0466759019477942));
#40138=CARTESIAN_POINT('',(0.00598790325387306,0.0478032051190145,0.0486214896541146));
#40139=CARTESIAN_POINT('',(0.00484431549305635,0.0477124908333002,0.0501955031725749));
#40140=CARTESIAN_POINT('',(0.00370072773223964,0.0476217765475859,0.0517695166910351));
#40141=CARTESIAN_POINT('',(0.00185036386611982,0.0475310622618717,0.0523707363563351));
#40142=CARTESIAN_POINT('',(1.15656637031819E-18,0.0474403479761574,0.0529719560216351));
#40143=CARTESIAN_POINT('',(-0.00185036386611982,0.0473496336904431,0.0523707363563351));
#40144=CARTESIAN_POINT('',(-0.00370072773223964,0.0472589194047288,0.0517695166910351));
#40145=CARTESIAN_POINT('',(-0.00484431549305635,0.0471682051190145,0.0501955031725749));
#40146=CARTESIAN_POINT('',(-0.00598790325387306,0.0470774908333002,0.0486214896541146));
#40147=CARTESIAN_POINT('',(-0.00598790325387306,0.0469867765475859,0.0466759019477942));
#40148=CARTESIAN_POINT('',(-0.00598790325387306,0.0468960622618716,0.0447303142414737));
#40149=CARTESIAN_POINT('',(-0.00484431549305635,0.0468053479761574,0.0431563007230135));
#40150=CARTESIAN_POINT('',(-0.00370072773223964,0.0467146336904431,0.0415822872045532));
#40151=CARTESIAN_POINT('',(-0.00185036386611982,0.0466239194047288,0.0409810675392532));
#40152=CARTESIAN_POINT('',(-3.85522123439397E-19,0.0465332051190145,0.0403798478739532));
#40153=CARTESIAN_POINT('',(0.00185036386611982,0.0464424908333002,0.0409810675392532));
#40154=CARTESIAN_POINT('',(0.00370072773223964,0.046351776547586,0.0415822872045532));
#40155=CARTESIAN_POINT('',(0.00484431549305635,0.0462610622618717,0.0431563007230135));
#40156=CARTESIAN_POINT('',(0.00598790325387306,0.0461703479761574,0.0447303142414737));
#40157=CARTESIAN_POINT('',(0.00598790325387306,0.0460796336904431,0.0466759019477942));
#40158=CARTESIAN_POINT('',(0.00598790325387306,0.0459889194047288,0.0486214896541146));
#40159=CARTESIAN_POINT('',(0.00484431549305635,0.0458982051190145,0.0501955031725749));
#40160=CARTESIAN_POINT('',(0.00370072773223964,0.0458074908333002,0.0517695166910351));
#40161=CARTESIAN_POINT('',(0.00185036386611982,0.045716776547586,0.0523707363563351));
#40162=CARTESIAN_POINT('',(1.15656637031819E-18,0.0456260622618716,0.0529719560216351));
#40163=CARTESIAN_POINT('',(-0.00185036386611982,0.0455353479761574,0.0523707363563351));
#40164=CARTESIAN_POINT('',(-0.00290461646238423,0.0454836631302826,0.0520281889230041));
#40165=CARTESIAN_POINT('',(-0.00376637754504363,0.0454293917687536,0.0513309406765197));
#40166=CARTESIAN_POINT('',(-0.00410750554856515,0.0454079084579156,0.0510549350560894));
#40167=CARTESIAN_POINT('',(-0.00444863355208667,0.0453864251470777,0.0507789294356591));
#40168=CARTESIAN_POINT('',(-0.00549100547232143,0.0527165177583816,0.0466759019477942));
#40169=CARTESIAN_POINT('',(-0.005,0.0529999999,0.0466759019477942));
#40170=CARTESIAN_POINT('',(-0.00598201094464286,0.0524330356167633,0.0466759019477942));
#40171=CARTESIAN_POINT('',(-0.005,0.0529999999,0.0466759019477942));
#40172=CARTESIAN_POINT('',(-0.005,0.0529092856142857,0.0450513034666297));
#40173=CARTESIAN_POINT('',(-0.00404508497187473,0.0528185713285714,0.0437369756863318));
#40174=CARTESIAN_POINT('',(-0.00309016994374947,0.0527278570428571,0.042422647906034));
#40175=CARTESIAN_POINT('',(-0.00154508497187473,0.0526371427571429,0.0419206193663185));
#40176=CARTESIAN_POINT('',(-0.000791922201622684,0.0525929234268318,0.0416759019477942));
#40177=CARTESIAN_POINT('',(-2.05609012588414E-18,0.0525464284714286,0.0416759019477942));
#40178=CARTESIAN_POINT('',(-2.05609012588413E-18,0.0525464284714286,0.0416759019477942));
#40179=CARTESIAN_POINT('',(-2.05609012588414E-18,0.0525464284714286,0.0416759019477942));
#40180=CARTESIAN_POINT('',(0.000791922201622679,0.0524999335160253,0.0416759019477942));
#40181=CARTESIAN_POINT('',(0.00154508497187473,0.0524557141857143,0.0419206193663185));
#40182=CARTESIAN_POINT('',(0.00309016994374947,0.0523649999,0.042422647906034));
#40183=CARTESIAN_POINT('',(0.00404508497187473,0.0522742856142857,0.0437369756863318));
#40184=CARTESIAN_POINT('',(0.005,0.0521835713285714,0.0450513034666296));
#40185=CARTESIAN_POINT('',(0.005,0.0520928570428571,0.0466759019477942));
#40186=CARTESIAN_POINT('',(0.005,0.0520021427571428,0.0483005004289586));
#40187=CARTESIAN_POINT('',(0.00404508497187473,0.0519114284714286,0.0496148282092566));
#40188=CARTESIAN_POINT('',(0.00309016994374947,0.0518207141857143,0.0509291559895544));
#40189=CARTESIAN_POINT('',(0.00154508497187474,0.0517299999,0.05143118452927));
#40190=CARTESIAN_POINT('',(0.000791922201622684,0.0516857805696889,0.0516759019477941));
#40191=CARTESIAN_POINT('',(4.44560027218191E-18,0.0516392856142857,0.0516759019477941));
#40192=CARTESIAN_POINT('',(4.44560027218192E-18,0.0516392856142857,0.0516759019477942));
#40193=CARTESIAN_POINT('',(4.44560027218191E-18,0.0516392856142857,0.0516759019477941));
#40194=CARTESIAN_POINT('',(-0.000791922201622684,0.0515927906588825,0.0516759019477942));
#40195=CARTESIAN_POINT('',(-0.00154508497187474,0.0515485713285714,0.05143118452927));
#40196=CARTESIAN_POINT('',(-0.00309016994374949,0.0514578570428571,0.0509291559895544));
#40197=CARTESIAN_POINT('',(-0.00404508497187476,0.0513671427571428,0.0496148282092566));
#40198=CARTESIAN_POINT('',(-0.00500000000000003,0.0512764284714286,0.0483005004289587));
#40199=CARTESIAN_POINT('',(-0.005,0.0511857141857143,0.0466759019477942));
#40200=CARTESIAN_POINT('',(-0.00500000000000003,0.0510949999,0.0450513034666296));
#40201=CARTESIAN_POINT('',(-0.00404508497187476,0.0510042856142857,0.0437369756863318));
#40202=CARTESIAN_POINT('',(-0.00309016994374949,0.0509135713285715,0.0424226479060339));
#40203=CARTESIAN_POINT('',(-0.00154508497187475,0.0508228570428571,0.0419206193663184));
#40204=CARTESIAN_POINT('',(-0.000791922201629948,0.0507786377125465,0.0416759019477965));
#40205=CARTESIAN_POINT('',(-1.49045973225341E-14,0.0507321427571437,0.0416759019477942));
#40206=CARTESIAN_POINT('',(-1.49045973225341E-14,0.0507321427571437,0.0416759019477942));
#40207=CARTESIAN_POINT('',(-1.49045973225341E-14,0.0507321427571437,0.0416759019477942));
#40208=CARTESIAN_POINT('',(0.000791922201615424,0.0506856478017401,0.0416759019477918));
#40209=CARTESIAN_POINT('',(0.00154508497187474,0.0506414284714286,0.0419206193663184));
#40210=CARTESIAN_POINT('',(0.00309016994374949,0.0505507141857142,0.0424226479060339));
#40211=CARTESIAN_POINT('',(0.00404508497187476,0.0504599999,0.0437369756863318));
#40212=CARTESIAN_POINT('',(0.00500000000000003,0.0503692856142857,0.0450513034666296));
#40213=CARTESIAN_POINT('',(0.005,0.0502785713285714,0.0466759019477942));
#40214=CARTESIAN_POINT('',(0.00500000000000003,0.0501878570428571,0.0483005004289587));
#40215=CARTESIAN_POINT('',(0.00404508497187476,0.0500971427571428,0.0496148282092566));
#40216=CARTESIAN_POINT('',(0.00309016994374949,0.0500064284714285,0.0509291559895544));
#40217=CARTESIAN_POINT('',(0.00154508497187475,0.0499157141857143,0.05143118452927));
#40218=CARTESIAN_POINT('',(0.000791922201622684,0.0498714948554032,0.0516759019477942));
#40219=CARTESIAN_POINT('',(-6.11270037425013E-18,0.0498249999,0.0516759019477941));
#40220=CARTESIAN_POINT('',(-6.11270037425013E-18,0.0498249999,0.0516759019477942));
#40221=CARTESIAN_POINT('',(-6.11270037425013E-18,0.0498249999,0.0516759019477941));
#40222=CARTESIAN_POINT('',(-0.000791922201622682,0.0497785049445967,0.0516759019477941));
#40223=CARTESIAN_POINT('',(-0.00154508497187473,0.0497342856142857,0.0514311845292699));
#40224=CARTESIAN_POINT('',(-0.00309016994374947,0.0496435713285714,0.0509291559895543));
#40225=CARTESIAN_POINT('',(-0.00404508497187473,0.0495528570428571,0.0496148282092566));
#40226=CARTESIAN_POINT('',(-0.00499999999999999,0.0494621427571428,0.0483005004289586));
#40227=CARTESIAN_POINT('',(-0.005,0.0493714284714286,0.0466759019477942));
#40228=CARTESIAN_POINT('',(-0.00499999999999999,0.0492807141857143,0.0450513034666297));
#40229=CARTESIAN_POINT('',(-0.00404508497187473,0.0491899999,0.0437369756863318));
#40230=CARTESIAN_POINT('',(-0.00309016994374947,0.0490992856142857,0.042422647906034));
#40231=CARTESIAN_POINT('',(-0.00154508497187473,0.0490085713285714,0.0419206193663185));
#40232=CARTESIAN_POINT('',(-0.00079192220162268,0.0489643519982604,0.0416759019477942));
#40233=CARTESIAN_POINT('',(-2.7785001701137E-19,0.0489178570428571,0.0416759019477942));
#40234=CARTESIAN_POINT('',(-2.77850017011369E-19,0.0489178570428571,0.0416759019477942));
#40235=CARTESIAN_POINT('',(-2.7785001701137E-19,0.0489178570428571,0.0416759019477942));
#40236=CARTESIAN_POINT('',(0.000791922201622679,0.048871362087454,0.0416759019477942));
#40237=CARTESIAN_POINT('',(0.00154508497187473,0.0488271427571429,0.0419206193663185));
#40238=CARTESIAN_POINT('',(0.00309016994374946,0.0487364284714286,0.042422647906034));
#40239=CARTESIAN_POINT('',(0.00404508497187472,0.0486457141857143,0.0437369756863318));
#40240=CARTESIAN_POINT('',(0.00499999999999998,0.0485549999,0.0450513034666297));
#40241=CARTESIAN_POINT('',(0.005,0.0484642856142857,0.0466759019477942));
#40242=CARTESIAN_POINT('',(0.00499999999999998,0.0483735713285714,0.0483005004289586));
#40243=CARTESIAN_POINT('',(0.00404508497187472,0.0482828570428572,0.0496148282092566));
#40244=CARTESIAN_POINT('',(0.00309016994374946,0.0481921427571428,0.0509291559895543));
#40245=CARTESIAN_POINT('',(0.00154508497187473,0.0481014284714286,0.0514311845292699));
#40246=CARTESIAN_POINT('',(0.000791922201633343,0.0480572091411181,0.0516759019477907));
#40247=CARTESIAN_POINT('',(2.18756875393391E-14,0.0480107141857156,0.0516759019477941));
#40248=CARTESIAN_POINT('',(2.18756875393391E-14,0.0480107141857156,0.0516759019477942));
#40249=CARTESIAN_POINT('',(2.18756875393391E-14,0.0480107141857156,0.0516759019477941));
#40250=CARTESIAN_POINT('',(-0.000791922201612015,0.0479642192303117,0.0516759019477976));
#40251=CARTESIAN_POINT('',(-0.00154508497187473,0.0479199999,0.0514311845292699));
#40252=CARTESIAN_POINT('',(-0.00309016994374946,0.0478292856142857,0.0509291559895543));
#40253=CARTESIAN_POINT('',(-0.00404508497187472,0.0477385713285714,0.0496148282092566));
#40254=CARTESIAN_POINT('',(-0.00499999999999998,0.0476478570428571,0.0483005004289586));
#40255=CARTESIAN_POINT('',(-0.005,0.0475571427571429,0.0466759019477942));
#40256=CARTESIAN_POINT('',(-0.00499999999999998,0.0474664284714286,0.0450513034666297));
#40257=CARTESIAN_POINT('',(-0.00404508497187472,0.0473757141857143,0.0437369756863318));
#40258=CARTESIAN_POINT('',(-0.00309016994374946,0.0472849999,0.042422647906034));
#40259=CARTESIAN_POINT('',(-0.00154508497187473,0.0471942856142857,0.0419206193663185));
#40260=CARTESIAN_POINT('',(-0.000791922201622666,0.0471500662839747,0.0416759019477942));
#40261=CARTESIAN_POINT('',(2.78405717045393E-17,0.0471035713285714,0.0416759019477942));
#40262=CARTESIAN_POINT('',(2.78405717045392E-17,0.0471035713285714,0.0416759019477942));
#40263=CARTESIAN_POINT('',(2.78405717045393E-17,0.0471035713285714,0.0416759019477942));
#40264=CARTESIAN_POINT('',(0.00079192220162271,0.0470570763731681,0.0416759019477941));
#40265=CARTESIAN_POINT('',(0.00154508497187477,0.0470128570428571,0.0419206193663183));
#40266=CARTESIAN_POINT('',(0.00309016994374953,0.0469221427571428,0.0424226479060339));
#40267=CARTESIAN_POINT('',(0.00404508497187482,0.0468314284714285,0.0437369756863317));
#40268=CARTESIAN_POINT('',(0.00500000000000009,0.0467407141857142,0.0450513034666296));
#40269=CARTESIAN_POINT('',(0.0050000000000001,0.0466499998999999,0.0466759019477942));
#40270=CARTESIAN_POINT('',(0.00500000000000009,0.0465592856142856,0.0483005004289587));
#40271=CARTESIAN_POINT('',(0.00404508497187482,0.0464685713285714,0.0496148282092566));
#40272=CARTESIAN_POINT('',(0.00309016994374953,0.0463778570428571,0.0509291559895544));
#40273=CARTESIAN_POINT('',(0.00154508497187477,0.0462871427571428,0.05143118452927));
#40274=CARTESIAN_POINT('',(0.000791922201622793,0.0462429234268318,0.0516759019477943));
#40275=CARTESIAN_POINT('',(1.83714431247917E-16,0.0461964284714285,0.0516759019477941));
#40276=CARTESIAN_POINT('',(1.83714431247917E-16,0.0461964284714286,0.0516759019477942));
#40277=CARTESIAN_POINT('',(1.83714431247918E-16,0.0461964284714286,0.0516759019477942));
#40278=CARTESIAN_POINT('',(-0.00114474007368374,0.0461292190428191,0.0516759019477942));
#40279=CARTESIAN_POINT('',(-0.00225506927301393,0.046066874298055,0.0512829728428846));
#40280=CARTESIAN_POINT('',(-0.0031449996694696,0.0459997571466553,0.0505629287137221));
#40281=CARTESIAN_POINT('',(-0.00314499966946895,0.045999757146644,0.0505629287137221));
#40282=CARTESIAN_POINT('',(-0.00345383548269564,0.0457162754208589,0.0509446443334947));
#40283=CARTESIAN_POINT('',(-0.00376267129592233,0.0454327936950738,0.0513263599532673));
#40284=CARTESIAN_POINT('',(-0.00598201094464286,0.0524330356167633,0.0466759019477942));
#40285=CARTESIAN_POINT('',(-0.00598201094464285,0.052342321331049,0.0447322287687989));
#40286=CARTESIAN_POINT('',(-0.004839548514753,0.0522516070453347,0.0431597641354809));
#40287=CARTESIAN_POINT('',(-0.00369708608486315,0.0521608927596204,0.041587299502163));
#40288=CARTESIAN_POINT('',(-0.00184854304243157,0.0520701784739062,0.0409866714583427));
#40289=CARTESIAN_POINT('',(-3.8514275599305E-19,0.0519794641881918,0.0403860434145223));
#40290=CARTESIAN_POINT('',(0.00184854304243157,0.0518887499024776,0.0409866714583427));
#40291=CARTESIAN_POINT('',(0.00369708608486315,0.0517980356167633,0.041587299502163));
#40292=CARTESIAN_POINT('',(0.004839548514753,0.051707321331049,0.0431597641354809));
#40293=CARTESIAN_POINT('',(0.00598201094464285,0.0516166070453347,0.0447322287687989));
#40294=CARTESIAN_POINT('',(0.00598201094464286,0.0515258927596204,0.0466759019477942));
#40295=CARTESIAN_POINT('',(0.00598201094464286,0.0514351784739062,0.0486195751267895));
#40296=CARTESIAN_POINT('',(0.004839548514753,0.0513444641881919,0.0501920397601074));
#40297=CARTESIAN_POINT('',(0.00369708608486315,0.0512537499024776,0.0517645043934253));
#40298=CARTESIAN_POINT('',(0.00184854304243157,0.0511630356167633,0.0523651324372457));
#40299=CARTESIAN_POINT('',(1.15542826797915E-18,0.051072321331049,0.052965760481066));
#40300=CARTESIAN_POINT('',(-0.00184854304243157,0.0509816070453347,0.0523651324372457));
#40301=CARTESIAN_POINT('',(-0.00369708608486315,0.0508908927596205,0.0517645043934253));
#40302=CARTESIAN_POINT('',(-0.004839548514753,0.0508001784739061,0.0501920397601074));
#40303=CARTESIAN_POINT('',(-0.00598201094464285,0.0507094641881918,0.0486195751267895));
#40304=CARTESIAN_POINT('',(-0.00598201094464286,0.0506187499024776,0.0466759019477942));
#40305=CARTESIAN_POINT('',(-0.00598201094464285,0.0505280356167632,0.0447322287687989));
#40306=CARTESIAN_POINT('',(-0.004839548514753,0.050437321331049,0.0431597641354809));
#40307=CARTESIAN_POINT('',(-0.00369708608486315,0.0503466070453347,0.041587299502163));
#40308=CARTESIAN_POINT('',(-0.00184854304243157,0.0502558927596204,0.0409866714583427));
#40309=CARTESIAN_POINT('',(-3.8514275599305E-19,0.0501651784739061,0.0403860434145223));
#40310=CARTESIAN_POINT('',(0.00184854304243157,0.0500744641881919,0.0409866714583427));
#40311=CARTESIAN_POINT('',(0.00369708608486315,0.0499837499024775,0.041587299502163));
#40312=CARTESIAN_POINT('',(0.004839548514753,0.0498930356167633,0.0431597641354809));
#40313=CARTESIAN_POINT('',(0.00598201094464285,0.049802321331049,0.0447322287687989));
#40314=CARTESIAN_POINT('',(0.00598201094464286,0.0497116070453347,0.0466759019477942));
#40315=CARTESIAN_POINT('',(0.00598201094464286,0.0496208927596204,0.0486195751267895));
#40316=CARTESIAN_POINT('',(0.004839548514753,0.0495301784739061,0.0501920397601074));
#40317=CARTESIAN_POINT('',(0.00369708608486315,0.0494394641881919,0.0517645043934253));
#40318=CARTESIAN_POINT('',(0.00184854304243157,0.0493487499024776,0.0523651324372457));
#40319=CARTESIAN_POINT('',(1.15542826797915E-18,0.0492580356167633,0.052965760481066));
#40320=CARTESIAN_POINT('',(-0.00184854304243157,0.049167321331049,0.0523651324372457));
#40321=CARTESIAN_POINT('',(-0.00369708608486315,0.0490766070453347,0.0517645043934253));
#40322=CARTESIAN_POINT('',(-0.004839548514753,0.0489858927596204,0.0501920397601074));
#40323=CARTESIAN_POINT('',(-0.00598201094464285,0.0488951784739062,0.0486195751267895));
#40324=CARTESIAN_POINT('',(-0.00598201094464286,0.0488044641881919,0.0466759019477942));
#40325=CARTESIAN_POINT('',(-0.00598201094464285,0.0487137499024776,0.0447322287687989));
#40326=CARTESIAN_POINT('',(-0.004839548514753,0.0486230356167633,0.0431597641354809));
#40327=CARTESIAN_POINT('',(-0.00369708608486315,0.0485323213310489,0.041587299502163));
#40328=CARTESIAN_POINT('',(-0.00184854304243157,0.0484416070453347,0.0409866714583427));
#40329=CARTESIAN_POINT('',(-3.8514275599305E-19,0.0483508927596204,0.0403860434145223));
#40330=CARTESIAN_POINT('',(0.00184854304243157,0.0482601784739061,0.0409866714583427));
#40331=CARTESIAN_POINT('',(0.00369708608486315,0.0481694641881918,0.041587299502163));
#40332=CARTESIAN_POINT('',(0.004839548514753,0.0480787499024776,0.0431597641354809));
#40333=CARTESIAN_POINT('',(0.00598201094464285,0.0479880356167633,0.0447322287687989));
#40334=CARTESIAN_POINT('',(0.00598201094464286,0.047897321331049,0.0466759019477942));
#40335=CARTESIAN_POINT('',(0.00598201094464286,0.0478066070453347,0.0486195751267895));
#40336=CARTESIAN_POINT('',(0.004839548514753,0.0477158927596204,0.0501920397601074));
#40337=CARTESIAN_POINT('',(0.00369708608486315,0.0476251784739061,0.0517645043934253));
#40338=CARTESIAN_POINT('',(0.00184854304243157,0.0475344641881919,0.0523651324372457));
#40339=CARTESIAN_POINT('',(1.15542826797915E-18,0.0474437499024775,0.052965760481066));
#40340=CARTESIAN_POINT('',(-0.00184854304243157,0.0473530356167633,0.0523651324372457));
#40341=CARTESIAN_POINT('',(-0.00369708608486315,0.047262321331049,0.0517645043934253));
#40342=CARTESIAN_POINT('',(-0.004839548514753,0.0471716070453347,0.0501920397601074));
#40343=CARTESIAN_POINT('',(-0.00598201094464285,0.0470808927596204,0.0486195751267895));
#40344=CARTESIAN_POINT('',(-0.00598201094464286,0.0469901784739061,0.0466759019477942));
#40345=CARTESIAN_POINT('',(-0.00598201094464285,0.0468994641881918,0.0447322287687989));
#40346=CARTESIAN_POINT('',(-0.004839548514753,0.0468087499024776,0.0431597641354809));
#40347=CARTESIAN_POINT('',(-0.00369708608486315,0.0467180356167633,0.041587299502163));
#40348=CARTESIAN_POINT('',(-0.00184854304243157,0.046627321331049,0.0409866714583427));
#40349=CARTESIAN_POINT('',(-3.8514275599305E-19,0.0465366070453347,0.0403860434145223));
#40350=CARTESIAN_POINT('',(0.00184854304243157,0.0464458927596204,0.0409866714583427));
#40351=CARTESIAN_POINT('',(0.00369708608486315,0.0463551784739062,0.041587299502163));
#40352=CARTESIAN_POINT('',(0.004839548514753,0.0462644641881919,0.0431597641354809));
#40353=CARTESIAN_POINT('',(0.00598201094464285,0.0461737499024775,0.0447322287687989));
#40354=CARTESIAN_POINT('',(0.00598201094464286,0.0460830356167633,0.0466759019477942));
#40355=CARTESIAN_POINT('',(0.00598201094464286,0.045992321331049,0.0486195751267895));
#40356=CARTESIAN_POINT('',(0.004839548514753,0.0459016070453347,0.0501920397601074));
#40357=CARTESIAN_POINT('',(0.00369708608486315,0.0458108927596204,0.0517645043934253));
#40358=CARTESIAN_POINT('',(0.00184854304243157,0.0457201784739062,0.0523651324372457));
#40359=CARTESIAN_POINT('',(1.15542826797915E-18,0.0456294641881918,0.052965760481066));
#40360=CARTESIAN_POINT('',(-0.00184854304243157,0.0455387499024776,0.0523651324372457));
#40361=CARTESIAN_POINT('',(-0.00290176072609409,0.0454870649334603,0.052022921267403));
#40362=CARTESIAN_POINT('',(-0.00376267129592233,0.0454327936950738,0.0513263599532673));
#40363=CARTESIAN_POINT('',(-0.00598201094464286,0.0524330356167633,0.0466759019477942));
#40364=CARTESIAN_POINT('',(-0.00598201094464285,0.0523981542391963,0.0459285224420255));
#40365=CARTESIAN_POINT('',(-0.00583674035853046,0.0523600126982779,0.0451584909126088));
#40366=CARTESIAN_POINT('',(-0.00526679477720715,0.0522850757530042,0.043738054600265));
#40367=CARTESIAN_POINT('',(-0.00485551285147822,0.0522505220626225,0.0431001763752942));
#40368=CARTESIAN_POINT('',(-0.00380735353003082,0.0521771690905066,0.0419998055503637));
#40369=CARTESIAN_POINT('',(-0.00316594922103819,0.0521385572455577,0.0415440076504345));
#40370=CARTESIAN_POINT('',(-0.00178519030427026,0.0520656343206208,0.0409163299908685));
#40371=CARTESIAN_POINT('',(-0.00104574457906955,0.0520307824265841,0.0407364425364496));
#40372=CARTESIAN_POINT('',(0.00124883818411648,0.0519181794567874,0.0406285820737455));
#40373=CARTESIAN_POINT('',(0.0027736318720953,0.0518470362547518,0.041159545998454));
#40374=CARTESIAN_POINT('',(0.00450401018390079,0.0517348984409267,0.0426655356739834));
#40375=CARTESIAN_POINT('',(0.00497090043471929,0.0517005528598357,0.0432621087295777));
#40376=CARTESIAN_POINT('',(0.00566742120758123,0.0516268132822675,0.0446157630873064));
#40377=CARTESIAN_POINT('',(0.00588684376001165,0.0515882271308646,0.0453712275482034));
#40378=CARTESIAN_POINT('',(0.0060262886549628,0.0515157768245541,0.0468782624943499));
#40379=CARTESIAN_POINT('',(0.00595354459638783,0.0514805372365184,0.0476384545546751));
#40380=CARTESIAN_POINT('',(0.00551892559300571,0.0514053838650747,0.049107498353668));
#40381=CARTESIAN_POINT('',(0.00516078841230873,0.0513687295160337,0.0497929457474596));
#40382=CARTESIAN_POINT('',(0.0042289612539199,0.0512976948409907,0.050973062149427));
#40383=CARTESIAN_POINT('',(0.00363547045728982,0.0512592942121183,0.0514874847945174));
#40384=CARTESIAN_POINT('',(0.00230967647504479,0.0511847604023482,0.0522466621757463));
#40385=CARTESIAN_POINT('',(0.00159375727545667,0.0511505324137917,0.052491876340922));
#40386=CARTESIAN_POINT('',(8.41419074369142E-5,0.051076450460237,0.0527057063006735));
#40387=CARTESIAN_POINT('',(-0.00070110682816806,0.0510379156376641,0.0526644631841532));
#40388=CARTESIAN_POINT('',(-0.0021669940603479,0.0509659795722588,0.0523024953406513));
#40389=CARTESIAN_POINT('',(-0.00286428837585678,0.050930263582991,0.0519831845300897));
#40390=CARTESIAN_POINT('',(-0.00473183918614788,0.0508174771686901,0.0506435105883454));
#40391=CARTESIAN_POINT('',(-0.00559797051942237,0.0507460599078541,0.049278904374021));
#40392=CARTESIAN_POINT('',(-0.00602010683490445,0.0506346650879708,0.0470292838863863));
#40393=CARTESIAN_POINT('',(-0.00601702730980891,0.0506004639362058,0.0462727235034844));
#40394=CARTESIAN_POINT('',(-0.00572295460377424,0.0505260845379958,0.0447745968412735));
#40395=CARTESIAN_POINT('',(-0.00542594286454709,0.0504876265632931,0.0440470889901856));
#40396=CARTESIAN_POINT('',(-0.00419473858185236,0.0503805547237801,0.0421529761750096));
#40397=CARTESIAN_POINT('',(-0.00285634696512304,0.0503053491211378,0.0412068905161621));
#40398=CARTESIAN_POINT('',(-0.000650935336709183,0.0501971220817964,0.0406815858567029));
#40399=CARTESIAN_POINT('',(0.000134804213528367,0.0501585631732825,0.040647075667539));
#40400=CARTESIAN_POINT('',(0.00164167590883445,0.0500846158610668,0.0408733319392693));
#40401=CARTESIAN_POINT('',(0.00235581443537718,0.0500503507357777,0.0411244497890724));
#40402=CARTESIAN_POINT('',(0.00433579048496438,0.0499384037879682,0.0422802806102534));
#40403=CARTESIAN_POINT('',(0.00532798133591556,0.0498672080706738,0.0435544519204082));
#40404=CARTESIAN_POINT('',(0.00596136440889945,0.0497545214563175,0.0457631125755893));
#40405=CARTESIAN_POINT('',(0.00602782510225254,0.0497194512071264,0.0465227163609867));
#40406=CARTESIAN_POINT('',(0.00587578144387195,0.0496468025108145,0.0480299084881039));
#40407=CARTESIAN_POINT('',(0.00564985425987283,0.0496082027476912,0.0487835511151446));
#40408=CARTESIAN_POINT('',(0.00494259057665489,0.0495346159913582,0.0501304404932439));
#40409=CARTESIAN_POINT('',(0.00447054501904416,0.0495001962123006,0.0507235904043108));
#40410=CARTESIAN_POINT('',(0.00330820369998183,0.0494253590792445,0.0517182568428551));
#40411=CARTESIAN_POINT('',(0.00262492815279643,0.0493871306061523,0.0521031329958861));
#40412=CARTESIAN_POINT('',(0.00120628154563118,0.0493169764065971,0.0525826751353633));
#40413=CARTESIAN_POINT('',(0.000433509776971783,0.049279309413946,0.0526910975554302));
#40414=CARTESIAN_POINT('',(-0.00109522981267062,0.0492042889698804,0.0526064146222846));
#40415=CARTESIAN_POINT('',(-0.00183230736936312,0.049169569897136,0.052420740389839));
#40416=CARTESIAN_POINT('',(-0.00320894594061515,0.0490964658838563,0.0517811134978896));
#40417=CARTESIAN_POINT('',(-0.00384643009871131,0.0490578509322671,0.0513198122705482));
#40418=CARTESIAN_POINT('',(-0.0048846195327673,0.0489846686492892,0.0502116366112216));
#40419=CARTESIAN_POINT('',(-0.00529110431748674,0.0489500038503849,0.0495697919341571));
#40420=CARTESIAN_POINT('',(-0.00612839681505211,0.0488375091393325,0.0474314972485811));
#40421=CARTESIAN_POINT('',(-0.00611457685600949,0.0487663945071744,0.0458171355611411));
#40422=CARTESIAN_POINT('',(-0.00524213722913385,0.0486540901028407,0.0436943384425134));
#40423=CARTESIAN_POINT('',(-0.00482603837135703,0.048619632447345,0.0430603764341383));
#40424=CARTESIAN_POINT('',(-0.00376799594300458,0.0485461160542431,0.0419679429765193));
#40425=CARTESIAN_POINT('',(-0.00312274344804228,0.048507511614782,0.0415176983874283));
#40426=CARTESIAN_POINT('',(-0.00173801800845273,0.0484347769007118,0.040902005168776));
#40427=CARTESIAN_POINT('',(-0.000996149780969905,0.04839977721282,0.0407279060321564));
#40428=CARTESIAN_POINT('',(0.000534394153117021,0.048324668223444,0.0406687901053457));
#40429=CARTESIAN_POINT('',(0.00130116707099782,0.0482876096687883,0.0407890711511285));
#40430=CARTESIAN_POINT('',(0.00271519543873335,0.0482169351067155,0.04129300994584));
#40431=CARTESIAN_POINT('',(0.00339241327145998,0.0481786006320457,0.0416898987444526));
#40432=CARTESIAN_POINT('',(0.00453713172897902,0.0481039284314745,0.0427031030072484));
#40433=CARTESIAN_POINT('',(0.00499890489099844,0.0480696419040328,0.0433031369857737));
#40434=CARTESIAN_POINT('',(0.00568458829322409,0.0479957569051978,0.0446634284610569));
#40435=CARTESIAN_POINT('',(0.00589748451337995,0.0479571886546133,0.0454206299072185));
#40436=CARTESIAN_POINT('',(0.00602435095420808,0.0478849437019996,0.0469273518671414));
#40437=CARTESIAN_POINT('',(0.00594530062534477,0.0478495199335978,0.0476881820089443));
#40438=CARTESIAN_POINT('',(0.00527488903437779,0.0477367582675181,0.0498864194514419));
#40439=CARTESIAN_POINT('',(0.00426061021221676,0.0476654504264648,0.0511439601596007));
#40440=CARTESIAN_POINT('',(0.00226342439943811,0.0475538074551243,0.0522655653621272));
#40441=CARTESIAN_POINT('',(0.00154567488468326,0.047519601418992,0.0525048960399918));
#40442=CARTESIAN_POINT('',(3.34690311347955E-5,0.0474453923415137,0.0527062554034359));
#40443=CARTESIAN_POINT('',(-0.000751201884539185,0.0474068858745274,0.0526582886400806));
#40444=CARTESIAN_POINT('',(-0.00294324433531448,0.0472993149061416,0.0520977989577606));
#40445=CARTESIAN_POINT('',(-0.00426698861795472,0.0472241498935822,0.0511318035742654));
#40446=CARTESIAN_POINT('',(-0.00546935161541402,0.0471163927702915,0.0492136365489639));
#40447=CARTESIAN_POINT('',(-0.00575400166720846,0.0470778700379339,0.0484807246240088));
#40448=CARTESIAN_POINT('',(-0.00602276831052684,0.047003730589497,0.0469795167638521));
#40449=CARTESIAN_POINT('',(-0.00601352874026243,0.0469695142442917,0.0462229028297622));
#40450=CARTESIAN_POINT('',(-0.00555346454973278,0.0468577822995324,0.0439783825107965));
#40451=CARTESIAN_POINT('',(-0.00466460616883524,0.0467865101593862,0.0426295328261682));
#40452=CARTESIAN_POINT('',(-0.00277511890321976,0.046673764575738,0.0413214673628862));
#40453=CARTESIAN_POINT('',(-0.00207521442244891,0.0466384448655614,0.0410146196892824));
#40454=CARTESIAN_POINT('',(-0.000600692686594825,0.0465660850757335,0.0406762519575071));
#40455=CARTESIAN_POINT('',(0.000185450487053797,0.0465275063600478,0.0406484824662403));
#40456=CARTESIAN_POINT('',(0.00168942626526117,0.0464537011603202,0.0408871182772802));
#40457=CARTESIAN_POINT('',(0.00240183301928324,0.0464193837266238,0.0411441618553943));
#40458=CARTESIAN_POINT('',(0.00371586134380875,0.0463446626465699,0.0419260256571976));
#40459=CARTESIAN_POINT('',(0.00429996898030531,0.0463063559145797,0.0424501078491));
#40460=CARTESIAN_POINT('',(0.00521018041629069,0.0462358232364466,0.0436425722548912));
#40461=CARTESIAN_POINT('',(0.00555890724136474,0.0461986014990264,0.0443372252724397));
#40462=CARTESIAN_POINT('',(0.00596876005678161,0.0461235139304544,0.0458129061804159));
#40463=CARTESIAN_POINT('',(0.00602895839985307,0.0460885981214,0.0465719721046274));
#40464=CARTESIAN_POINT('',(0.00586429821692855,0.0460157580652985,0.0480791650102269));
#40465=CARTESIAN_POINT('',(0.00563188957955514,0.0459771489847168,0.048830901324237));
#40466=CARTESIAN_POINT('',(0.00491397942628084,0.0459037223973798,0.0501708996225944));
#40467=CARTESIAN_POINT('',(0.0044367389074107,0.0458692133012517,0.0507606627917028));
#40468=CARTESIAN_POINT('',(0.0026802632123916,0.0457568513841524,0.052238501827766));
#40469=CARTESIAN_POINT('',(0.00114679585513747,0.0456857413559239,0.0527432212211965));
#40470=CARTESIAN_POINT('',(-0.00114460042476067,0.0455732947576852,0.0525970595245437));
#40471=CARTESIAN_POINT('',(-0.00187936400588002,0.0455386934886813,0.052405598071758));
#40472=CARTESIAN_POINT('',(-0.00290863757287697,0.045483735050253,0.0519169443403826));
#40473=CARTESIAN_POINT('',(-0.00323913157385276,0.0454649226491852,0.0517196323634921));
#40474=CARTESIAN_POINT('',(-0.00385599157597277,0.0454273273408982,0.0512652939363906));
#40475=CARTESIAN_POINT('',(-0.00414665186685566,0.045408587811407,0.0510156819102021));
#40476=CARTESIAN_POINT('',(-0.00444424750172291,0.0453898275775236,0.0507748977756262));
#40477=CARTESIAN_POINT('',(-0.00598201094464286,0.0523574403786681,0.0466759019477942));
#40478=CARTESIAN_POINT('',(-0.00598201094464285,0.0523225590011011,0.0459285224420255));
#40479=CARTESIAN_POINT('',(-0.00583674035853046,0.0522844174601826,0.0451584909126088));
#40480=CARTESIAN_POINT('',(-0.00526679477720715,0.0522094805149089,0.043738054600265));
#40481=CARTESIAN_POINT('',(-0.00485551285147822,0.0521749268245272,0.0431001763752942));
#40482=CARTESIAN_POINT('',(-0.00380735353003082,0.0521015738524114,0.0419998055503637));
#40483=CARTESIAN_POINT('',(-0.00316594922103819,0.0520629620074624,0.0415440076504345));
#40484=CARTESIAN_POINT('',(-0.00178519030427026,0.0519900390825255,0.0409163299908685));
#40485=CARTESIAN_POINT('',(-0.00104574457906955,0.0519551871884889,0.0407364425364496));
#40486=CARTESIAN_POINT('',(0.00124883818411648,0.0518425842186922,0.0406285820737455));
#40487=CARTESIAN_POINT('',(0.0027736318720953,0.0517714410166565,0.041159545998454));
#40488=CARTESIAN_POINT('',(0.00450401018390079,0.0516593032028314,0.0426655356739834));
#40489=CARTESIAN_POINT('',(0.00497090043471929,0.0516249576217405,0.0432621087295777));
#40490=CARTESIAN_POINT('',(0.00566742120758123,0.0515512180441723,0.0446157630873064));
#40491=CARTESIAN_POINT('',(0.00588684376001165,0.0515126318927694,0.0453712275482034));
#40492=CARTESIAN_POINT('',(0.0060262886549628,0.0514401815864589,0.0468782624943499));
#40493=CARTESIAN_POINT('',(0.00595354459638783,0.0514049419984231,0.0476384545546751));
#40494=CARTESIAN_POINT('',(0.00551892559300571,0.0513297886269795,0.049107498353668));
#40495=CARTESIAN_POINT('',(0.00516078841230873,0.0512931342779384,0.0497929457474596));
#40496=CARTESIAN_POINT('',(0.0042289612539199,0.0512220996028955,0.050973062149427));
#40497=CARTESIAN_POINT('',(0.00363547045728982,0.0511836989740231,0.0514874847945174));
#40498=CARTESIAN_POINT('',(0.00230967647504479,0.051109165164253,0.0522466621757463));
#40499=CARTESIAN_POINT('',(0.00159375727545667,0.0510749371756964,0.052491876340922));
#40500=CARTESIAN_POINT('',(8.41419074369142E-5,0.0510008552221417,0.0527057063006735));
#40501=CARTESIAN_POINT('',(-0.00070110682816806,0.0509623203995689,0.0526644631841532));
#40502=CARTESIAN_POINT('',(-0.0021669940603479,0.0508903843341635,0.0523024953406513));
#40503=CARTESIAN_POINT('',(-0.00286428837585678,0.0508546683448957,0.0519831845300897));
#40504=CARTESIAN_POINT('',(-0.00473183918614788,0.0507418819305949,0.0506435105883454));
#40505=CARTESIAN_POINT('',(-0.00559797051942237,0.0506704646697589,0.049278904374021));
#40506=CARTESIAN_POINT('',(-0.00602010683490445,0.0505590698498755,0.0470292838863863));
#40507=CARTESIAN_POINT('',(-0.00601702730980891,0.0505248686981106,0.0462727235034844));
#40508=CARTESIAN_POINT('',(-0.00572295460377424,0.0504504892999005,0.0447745968412735));
#40509=CARTESIAN_POINT('',(-0.00542594286454709,0.0504120313251979,0.0440470889901856));
#40510=CARTESIAN_POINT('',(-0.00419473858185236,0.0503049594856848,0.0421529761750096));
#40511=CARTESIAN_POINT('',(-0.00285634696512304,0.0502297538830426,0.0412068905161621));
#40512=CARTESIAN_POINT('',(-0.000650935336709183,0.0501215268437012,0.0406815858567029));
#40513=CARTESIAN_POINT('',(0.000134804213528367,0.0500829679351872,0.040647075667539));
#40514=CARTESIAN_POINT('',(0.00164167590883445,0.0500090206229716,0.0408733319392693));
#40515=CARTESIAN_POINT('',(0.00235581443537718,0.0499747554976825,0.0411244497890724));
#40516=CARTESIAN_POINT('',(0.00433579048496438,0.049862808549873,0.0422802806102534));
#40517=CARTESIAN_POINT('',(0.00532798133591556,0.0497916128325786,0.0435544519204082));
#40518=CARTESIAN_POINT('',(0.00596136440889945,0.0496789262182223,0.0457631125755893));
#40519=CARTESIAN_POINT('',(0.00602782510225254,0.0496438559690311,0.0465227163609867));
#40520=CARTESIAN_POINT('',(0.00587578144387195,0.0495712072727193,0.0480299084881039));
#40521=CARTESIAN_POINT('',(0.00564985425987283,0.049532607509596,0.0487835511151446));
#40522=CARTESIAN_POINT('',(0.00494259057665489,0.0494590207532629,0.0501304404932439));
#40523=CARTESIAN_POINT('',(0.00447054501904416,0.0494246009742053,0.0507235904043108));
#40524=CARTESIAN_POINT('',(0.00330820369998183,0.0493497638411493,0.0517182568428551));
#40525=CARTESIAN_POINT('',(0.00262492815279643,0.049311535368057,0.0521031329958861));
#40526=CARTESIAN_POINT('',(0.00120628154563118,0.0492413811685019,0.0525826751353633));
#40527=CARTESIAN_POINT('',(0.000433509776971783,0.0492037141758507,0.0526910975554302));
#40528=CARTESIAN_POINT('',(-0.00109522981267062,0.0491286937317851,0.0526064146222846));
#40529=CARTESIAN_POINT('',(-0.00183230736936312,0.0490939746590407,0.052420740389839));
#40530=CARTESIAN_POINT('',(-0.00320894594061515,0.0490208706457611,0.0517811134978896));
#40531=CARTESIAN_POINT('',(-0.00384643009871131,0.0489822556941719,0.0513198122705482));
#40532=CARTESIAN_POINT('',(-0.0048846195327673,0.048909073411194,0.0502116366112216));
#40533=CARTESIAN_POINT('',(-0.00529110431748674,0.0488744086122897,0.0495697919341571));
#40534=CARTESIAN_POINT('',(-0.00612839681505211,0.0487619139012373,0.0474314972485811));
#40535=CARTESIAN_POINT('',(-0.00611457685600949,0.0486907992690792,0.0458171355611411));
#40536=CARTESIAN_POINT('',(-0.00524213722913385,0.0485784948647455,0.0436943384425134));
#40537=CARTESIAN_POINT('',(-0.00482603837135703,0.0485440372092498,0.0430603764341383));
#40538=CARTESIAN_POINT('',(-0.00376799594300458,0.0484705208161479,0.0419679429765193));
#40539=CARTESIAN_POINT('',(-0.00312274344804228,0.0484319163766868,0.0415176983874283));
#40540=CARTESIAN_POINT('',(-0.00173801800845273,0.0483591816626165,0.040902005168776));
#40541=CARTESIAN_POINT('',(-0.000996149780969905,0.0483241819747248,0.0407279060321564));
#40542=CARTESIAN_POINT('',(0.000534394153117021,0.0482490729853488,0.0406687901053457));
#40543=CARTESIAN_POINT('',(0.00130116707099782,0.0482120144306931,0.0407890711511285));
#40544=CARTESIAN_POINT('',(0.00271519543873335,0.0481413398686203,0.04129300994584));
#40545=CARTESIAN_POINT('',(0.00339241327145998,0.0481030053939505,0.0416898987444526));
#40546=CARTESIAN_POINT('',(0.00453713172897902,0.0480283331933793,0.0427031030072484));
#40547=CARTESIAN_POINT('',(0.00499890489099844,0.0479940466659375,0.0433031369857737));
#40548=CARTESIAN_POINT('',(0.00568458829322409,0.0479201616671026,0.0446634284610569));
#40549=CARTESIAN_POINT('',(0.00589748451337995,0.047881593416518,0.0454206299072185));
#40550=CARTESIAN_POINT('',(0.00602435095420808,0.0478093484639044,0.0469273518671414));
#40551=CARTESIAN_POINT('',(0.00594530062534477,0.0477739246955026,0.0476881820089443));
#40552=CARTESIAN_POINT('',(0.00527488903437779,0.0476611630294229,0.0498864194514419));
#40553=CARTESIAN_POINT('',(0.00426061021221676,0.0475898551883695,0.0511439601596007));
#40554=CARTESIAN_POINT('',(0.00226342439943811,0.0474782122170291,0.0522655653621272));
#40555=CARTESIAN_POINT('',(0.00154567488468326,0.0474440061808968,0.0525048960399918));
#40556=CARTESIAN_POINT('',(3.34690311347955E-5,0.0473697971034185,0.0527062554034359));
#40557=CARTESIAN_POINT('',(-0.000751201884539185,0.0473312906364322,0.0526582886400806));
#40558=CARTESIAN_POINT('',(-0.00294324433531448,0.0472237196680463,0.0520977989577606));
#40559=CARTESIAN_POINT('',(-0.00426698861795472,0.047148554655487,0.0511318035742654));
#40560=CARTESIAN_POINT('',(-0.00546935161541402,0.0470407975321963,0.0492136365489639));
#40561=CARTESIAN_POINT('',(-0.00575400166720846,0.0470022747998386,0.0484807246240088));
#40562=CARTESIAN_POINT('',(-0.00602276831052684,0.0469281353514017,0.0469795167638521));
#40563=CARTESIAN_POINT('',(-0.00601352874026243,0.0468939190061965,0.0462229028297622));
#40564=CARTESIAN_POINT('',(-0.00555346454973278,0.0467821870614371,0.0439783825107965));
#40565=CARTESIAN_POINT('',(-0.00466460616883524,0.046710914921291,0.0426295328261682));
#40566=CARTESIAN_POINT('',(-0.00277511890321976,0.0465981693376428,0.0413214673628862));
#40567=CARTESIAN_POINT('',(-0.00207521442244891,0.0465628496274662,0.0410146196892824));
#40568=CARTESIAN_POINT('',(-0.000600692686594825,0.0464904898376383,0.0406762519575071));
#40569=CARTESIAN_POINT('',(0.000185450487053797,0.0464519111219526,0.0406484824662403));
#40570=CARTESIAN_POINT('',(0.00168942626526117,0.046378105922225,0.0408871182772802));
#40571=CARTESIAN_POINT('',(0.00240183301928324,0.0463437884885285,0.0411441618553943));
#40572=CARTESIAN_POINT('',(0.00371586134380875,0.0462690674084746,0.0419260256571976));
#40573=CARTESIAN_POINT('',(0.00429996898030531,0.0462307606764845,0.0424501078491));
#40574=CARTESIAN_POINT('',(0.00521018041629069,0.0461602279983514,0.0436425722548912));
#40575=CARTESIAN_POINT('',(0.00555890724136474,0.0461230062609312,0.0443372252724397));
#40576=CARTESIAN_POINT('',(0.00596876005678161,0.0460479186923591,0.0458129061804159));
#40577=CARTESIAN_POINT('',(0.00602895839985307,0.0460130028833048,0.0465719721046274));
#40578=CARTESIAN_POINT('',(0.00586429821692855,0.0459401628272032,0.0480791650102269));
#40579=CARTESIAN_POINT('',(0.00563188957955514,0.0459015537466216,0.048830901324237));
#40580=CARTESIAN_POINT('',(0.00491397942628084,0.0458281271592846,0.0501708996225944));
#40581=CARTESIAN_POINT('',(0.0044367389074107,0.0457936180631564,0.0507606627917028));
#40582=CARTESIAN_POINT('',(0.0026802632123916,0.0456812561460572,0.052238501827766));
#40583=CARTESIAN_POINT('',(0.00114679585513747,0.0456101461178287,0.0527432212211965));
#40584=CARTESIAN_POINT('',(-0.00114460042476067,0.04549769951959,0.0525970595245437));
#40585=CARTESIAN_POINT('',(-0.00187936400588002,0.0454630982505861,0.052405598071758));
#40586=CARTESIAN_POINT('',(-0.00290863757287697,0.0454081398121578,0.0519169443403826));
#40587=CARTESIAN_POINT('',(-0.00323913157385276,0.04538932741109,0.0517196323634921));
#40588=CARTESIAN_POINT('',(-0.00385599157597277,0.0453517321028029,0.0512652939363906));
#40589=CARTESIAN_POINT('',(-0.00414665186685566,0.0453329925733117,0.0510156819102021));
#40590=CARTESIAN_POINT('',(-0.00444424750172291,0.0453142323394283,0.0507748977756262));
#40591=CARTESIAN_POINT('',(-0.00598201094464286,0.0522818451405728,0.0466759019477942));
#40592=CARTESIAN_POINT('',(-0.00598201094464285,0.0522469637630059,0.0459285224420255));
#40593=CARTESIAN_POINT('',(-0.00583674035853046,0.0522088222220874,0.0451584909126088));
#40594=CARTESIAN_POINT('',(-0.00526679477720715,0.0521338852768137,0.043738054600265));
#40595=CARTESIAN_POINT('',(-0.00485551285147822,0.052099331586432,0.0431001763752942));
#40596=CARTESIAN_POINT('',(-0.00380735353003082,0.0520259786143161,0.0419998055503637));
#40597=CARTESIAN_POINT('',(-0.00316594922103819,0.0519873667693672,0.0415440076504345));
#40598=CARTESIAN_POINT('',(-0.00178519030427026,0.0519144438444302,0.0409163299908685));
#40599=CARTESIAN_POINT('',(-0.00104574457906955,0.0518795919503936,0.0407364425364496));
#40600=CARTESIAN_POINT('',(0.00124883818411648,0.051766988980597,0.0406285820737455));
#40601=CARTESIAN_POINT('',(0.0027736318720953,0.0516958457785613,0.041159545998454));
#40602=CARTESIAN_POINT('',(0.00450401018390079,0.0515837079647362,0.0426655356739834));
#40603=CARTESIAN_POINT('',(0.00497090043471929,0.0515493623836453,0.0432621087295777));
#40604=CARTESIAN_POINT('',(0.00566742120758123,0.051475622806077,0.0446157630873064));
#40605=CARTESIAN_POINT('',(0.00588684376001165,0.0514370366546741,0.0453712275482034));
#40606=CARTESIAN_POINT('',(0.0060262886549628,0.0513645863483636,0.0468782624943499));
#40607=CARTESIAN_POINT('',(0.00595354459638783,0.0513293467603279,0.0476384545546751));
#40608=CARTESIAN_POINT('',(0.00551892559300571,0.0512541933888842,0.049107498353668));
#40609=CARTESIAN_POINT('',(0.00516078841230873,0.0512175390398432,0.0497929457474596));
#40610=CARTESIAN_POINT('',(0.0042289612539199,0.0511465043648003,0.050973062149427));
#40611=CARTESIAN_POINT('',(0.00363547045728982,0.0511081037359278,0.0514874847945174));
#40612=CARTESIAN_POINT('',(0.00230967647504479,0.0510335699261577,0.0522466621757463));
#40613=CARTESIAN_POINT('',(0.00159375727545667,0.0509993419376012,0.052491876340922));
#40614=CARTESIAN_POINT('',(8.41419074369142E-5,0.0509252599840465,0.0527057063006735));
#40615=CARTESIAN_POINT('',(-0.00070110682816806,0.0508867251614736,0.0526644631841532));
#40616=CARTESIAN_POINT('',(-0.0021669940603479,0.0508147890960683,0.0523024953406513));
#40617=CARTESIAN_POINT('',(-0.00286428837585678,0.0507790731068005,0.0519831845300897));
#40618=CARTESIAN_POINT('',(-0.00473183918614788,0.0506662866924996,0.0506435105883454));
#40619=CARTESIAN_POINT('',(-0.00559797051942237,0.0505948694316636,0.049278904374021));
#40620=CARTESIAN_POINT('',(-0.00602010683490445,0.0504834746117803,0.0470292838863863));
#40621=CARTESIAN_POINT('',(-0.00601702730980891,0.0504492734600153,0.0462727235034844));
#40622=CARTESIAN_POINT('',(-0.00572295460377424,0.0503748940618053,0.0447745968412735));
#40623=CARTESIAN_POINT('',(-0.00542594286454709,0.0503364360871027,0.0440470889901856));
#40624=CARTESIAN_POINT('',(-0.00419473858185236,0.0502293642475896,0.0421529761750096));
#40625=CARTESIAN_POINT('',(-0.00285634696512304,0.0501541586449474,0.0412068905161621));
#40626=CARTESIAN_POINT('',(-0.000650935336709183,0.0500459316056059,0.0406815858567029));
#40627=CARTESIAN_POINT('',(0.000134804213528367,0.050007372697092,0.040647075667539));
#40628=CARTESIAN_POINT('',(0.00164167590883445,0.0499334253848764,0.0408733319392693));
#40629=CARTESIAN_POINT('',(0.00235581443537718,0.0498991602595873,0.0411244497890724));
#40630=CARTESIAN_POINT('',(0.00433579048496438,0.0497872133117777,0.0422802806102534));
#40631=CARTESIAN_POINT('',(0.00532798133591556,0.0497160175944833,0.0435544519204082));
#40632=CARTESIAN_POINT('',(0.00596136440889945,0.049603330980127,0.0457631125755893));
#40633=CARTESIAN_POINT('',(0.00602782510225254,0.0495682607309359,0.0465227163609867));
#40634=CARTESIAN_POINT('',(0.00587578144387195,0.049495612034624,0.0480299084881039));
#40635=CARTESIAN_POINT('',(0.00564985425987283,0.0494570122715007,0.0487835511151446));
#40636=CARTESIAN_POINT('',(0.00494259057665489,0.0493834255151677,0.0501304404932439));
#40637=CARTESIAN_POINT('',(0.00447054501904416,0.0493490057361101,0.0507235904043108));
#40638=CARTESIAN_POINT('',(0.00330820369998183,0.0492741686030541,0.0517182568428551));
#40639=CARTESIAN_POINT('',(0.00262492815279643,0.0492359401299618,0.0521031329958861));
#40640=CARTESIAN_POINT('',(0.00120628154563118,0.0491657859304066,0.0525826751353633));
#40641=CARTESIAN_POINT('',(0.000433509776971783,0.0491281189377555,0.0526910975554302));
#40642=CARTESIAN_POINT('',(-0.00109522981267062,0.0490530984936899,0.0526064146222846));
#40643=CARTESIAN_POINT('',(-0.00183230736936312,0.0490183794209455,0.052420740389839));
#40644=CARTESIAN_POINT('',(-0.00320894594061515,0.0489452754076659,0.0517811134978896));
#40645=CARTESIAN_POINT('',(-0.00384643009871131,0.0489066604560766,0.0513198122705482));
#40646=CARTESIAN_POINT('',(-0.0048846195327673,0.0488334781730987,0.0502116366112216));
#40647=CARTESIAN_POINT('',(-0.00529110431748674,0.0487988133741944,0.0495697919341571));
#40648=CARTESIAN_POINT('',(-0.00612839681505211,0.0486863186631421,0.0474314972485811));
#40649=CARTESIAN_POINT('',(-0.00611457685600949,0.0486152040309839,0.0458171355611411));
#40650=CARTESIAN_POINT('',(-0.00524213722913385,0.0485028996266502,0.0436943384425134));
#40651=CARTESIAN_POINT('',(-0.00482603837135703,0.0484684419711546,0.0430603764341383));
#40652=CARTESIAN_POINT('',(-0.00376799594300458,0.0483949255780527,0.0419679429765193));
#40653=CARTESIAN_POINT('',(-0.00312274344804228,0.0483563211385916,0.0415176983874283));
#40654=CARTESIAN_POINT('',(-0.00173801800845273,0.0482835864245213,0.040902005168776));
#40655=CARTESIAN_POINT('',(-0.000996149780969905,0.0482485867366295,0.0407279060321564));
#40656=CARTESIAN_POINT('',(0.000534394153117021,0.0481734777472535,0.0406687901053457));
#40657=CARTESIAN_POINT('',(0.00130116707099782,0.0481364191925979,0.0407890711511285));
#40658=CARTESIAN_POINT('',(0.00271519543873335,0.0480657446305251,0.04129300994584));
#40659=CARTESIAN_POINT('',(0.00339241327145998,0.0480274101558552,0.0416898987444526));
#40660=CARTESIAN_POINT('',(0.00453713172897902,0.047952737955284,0.0427031030072484));
#40661=CARTESIAN_POINT('',(0.00499890489099844,0.0479184514278423,0.0433031369857737));
#40662=CARTESIAN_POINT('',(0.00568458829322409,0.0478445664290073,0.0446634284610569));
#40663=CARTESIAN_POINT('',(0.00589748451337995,0.0478059981784228,0.0454206299072185));
#40664=CARTESIAN_POINT('',(0.00602435095420808,0.0477337532258091,0.0469273518671414));
#40665=CARTESIAN_POINT('',(0.00594530062534477,0.0476983294574074,0.0476881820089443));
#40666=CARTESIAN_POINT('',(0.00527488903437779,0.0475855677913276,0.0498864194514419));
#40667=CARTESIAN_POINT('',(0.00426061021221676,0.0475142599502743,0.0511439601596007));
#40668=CARTESIAN_POINT('',(0.00226342439943811,0.0474026169789338,0.0522655653621272));
#40669=CARTESIAN_POINT('',(0.00154567488468326,0.0473684109428015,0.0525048960399918));
#40670=CARTESIAN_POINT('',(3.34690311347955E-5,0.0472942018653233,0.0527062554034359));
#40671=CARTESIAN_POINT('',(-0.000751201884539185,0.047255695398337,0.0526582886400806));
#40672=CARTESIAN_POINT('',(-0.00294324433531448,0.0471481244299511,0.0520977989577606));
#40673=CARTESIAN_POINT('',(-0.00426698861795472,0.0470729594173918,0.0511318035742654));
#40674=CARTESIAN_POINT('',(-0.00546935161541402,0.0469652022941011,0.0492136365489639));
#40675=CARTESIAN_POINT('',(-0.00575400166720846,0.0469266795617434,0.0484807246240088));
#40676=CARTESIAN_POINT('',(-0.00602276831052684,0.0468525401133065,0.0469795167638521));
#40677=CARTESIAN_POINT('',(-0.00601352874026243,0.0468183237681012,0.0462229028297622));
#40678=CARTESIAN_POINT('',(-0.00555346454973278,0.0467065918233419,0.0439783825107965));
#40679=CARTESIAN_POINT('',(-0.00466460616883524,0.0466353196831958,0.0426295328261682));
#40680=CARTESIAN_POINT('',(-0.00277511890321976,0.0465225740995476,0.0413214673628862));
#40681=CARTESIAN_POINT('',(-0.00207521442244891,0.0464872543893709,0.0410146196892824));
#40682=CARTESIAN_POINT('',(-0.000600692686594825,0.046414894599543,0.0406762519575071));
#40683=CARTESIAN_POINT('',(0.000185450487053797,0.0463763158838573,0.0406484824662403));
#40684=CARTESIAN_POINT('',(0.00168942626526117,0.0463025106841298,0.0408871182772802));
#40685=CARTESIAN_POINT('',(0.00240183301928324,0.0462681932504333,0.0411441618553943));
#40686=CARTESIAN_POINT('',(0.00371586134380875,0.0461934721703794,0.0419260256571976));
#40687=CARTESIAN_POINT('',(0.00429996898030531,0.0461551654383893,0.0424501078491));
#40688=CARTESIAN_POINT('',(0.00521018041629069,0.0460846327602562,0.0436425722548912));
#40689=CARTESIAN_POINT('',(0.00555890724136474,0.046047411022836,0.0443372252724397));
#40690=CARTESIAN_POINT('',(0.00596876005678161,0.0459723234542639,0.0458129061804159));
#40691=CARTESIAN_POINT('',(0.00602895839985307,0.0459374076452096,0.0465719721046274));
#40692=CARTESIAN_POINT('',(0.00586429821692855,0.045864567589108,0.0480791650102269));
#40693=CARTESIAN_POINT('',(0.00563188957955514,0.0458259585085263,0.048830901324237));
#40694=CARTESIAN_POINT('',(0.00491397942628084,0.0457525319211894,0.0501708996225944));
#40695=CARTESIAN_POINT('',(0.0044367389074107,0.0457180228250612,0.0507606627917028));
#40696=CARTESIAN_POINT('',(0.0026802632123916,0.0456056609079619,0.052238501827766));
#40697=CARTESIAN_POINT('',(0.00114679585513747,0.0455345508797335,0.0527432212211965));
#40698=CARTESIAN_POINT('',(-0.00114460042476067,0.0454221042814947,0.0525970595245437));
#40699=CARTESIAN_POINT('',(-0.00187936400588002,0.0453875030124909,0.052405598071758));
#40700=CARTESIAN_POINT('',(-0.00290863757287697,0.0453325445740626,0.0519169443403826));
#40701=CARTESIAN_POINT('',(-0.00323913157385276,0.0453137321729947,0.0517196323634921));
#40702=CARTESIAN_POINT('',(-0.00385599157597277,0.0452761368647077,0.0512652939363906));
#40703=CARTESIAN_POINT('',(-0.00414665186685566,0.0452573973352165,0.0510156819102021));
#40704=CARTESIAN_POINT('',(-0.00444424750172291,0.0452386371013331,0.0507748977756262));
#40705=CARTESIAN_POINT('',(-0.00598201094464286,0.0522062499024776,0.0466759019477942));
#40706=CARTESIAN_POINT('',(-0.00598201094464285,0.0521713685249106,0.0459285224420255));
#40707=CARTESIAN_POINT('',(-0.00583674035853046,0.0521332269839922,0.0451584909126088));
#40708=CARTESIAN_POINT('',(-0.00526679477720715,0.0520582900387185,0.043738054600265));
#40709=CARTESIAN_POINT('',(-0.00485551285147822,0.0520237363483368,0.0431001763752942));
#40710=CARTESIAN_POINT('',(-0.00380735353003082,0.0519503833762209,0.0419998055503637));
#40711=CARTESIAN_POINT('',(-0.00316594922103819,0.0519117715312719,0.0415440076504345));
#40712=CARTESIAN_POINT('',(-0.00178519030427026,0.051838848606335,0.0409163299908685));
#40713=CARTESIAN_POINT('',(-0.00104574457906955,0.0518039967122984,0.0407364425364496));
#40714=CARTESIAN_POINT('',(0.00124883818411648,0.0516913937425018,0.0406285820737455));
#40715=CARTESIAN_POINT('',(0.0027736318720953,0.051620250540466,0.041159545998454));
#40716=CARTESIAN_POINT('',(0.00450401018390079,0.0515081127266409,0.0426655356739834));
#40717=CARTESIAN_POINT('',(0.00497090043471929,0.05147376714555,0.0432621087295777));
#40718=CARTESIAN_POINT('',(0.00566742120758123,0.0514000275679818,0.0446157630873064));
#40719=CARTESIAN_POINT('',(0.00588684376001165,0.0513614414165789,0.0453712275482034));
#40720=CARTESIAN_POINT('',(0.0060262886549628,0.0512889911102684,0.0468782624943499));
#40721=CARTESIAN_POINT('',(0.00595354459638783,0.0512537515222327,0.0476384545546751));
#40722=CARTESIAN_POINT('',(0.00551892559300571,0.051178598150789,0.049107498353668));
#40723=CARTESIAN_POINT('',(0.00516078841230873,0.051141943801748,0.0497929457474596));
#40724=CARTESIAN_POINT('',(0.0042289612539199,0.051070909126705,0.050973062149427));
#40725=CARTESIAN_POINT('',(0.00363547045728982,0.0510325084978326,0.0514874847945174));
#40726=CARTESIAN_POINT('',(0.00230967647504479,0.0509579746880625,0.0522466621757463));
#40727=CARTESIAN_POINT('',(0.00159375727545667,0.050923746699506,0.052491876340922));
#40728=CARTESIAN_POINT('',(8.41419074369142E-5,0.0508496647459513,0.0527057063006735));
#40729=CARTESIAN_POINT('',(-0.00070110682816806,0.0508111299233784,0.0526644631841532));
#40730=CARTESIAN_POINT('',(-0.0021669940603479,0.0507391938579731,0.0523024953406513));
#40731=CARTESIAN_POINT('',(-0.00286428837585678,0.0507034778687052,0.0519831845300897));
#40732=CARTESIAN_POINT('',(-0.00473183918614788,0.0505906914544044,0.0506435105883454));
#40733=CARTESIAN_POINT('',(-0.00559797051942237,0.0505192741935684,0.049278904374021));
#40734=CARTESIAN_POINT('',(-0.00602010683490445,0.0504078793736851,0.0470292838863863));
#40735=CARTESIAN_POINT('',(-0.00601702730980891,0.0503736782219201,0.0462727235034844));
#40736=CARTESIAN_POINT('',(-0.00572295460377424,0.0502992988237101,0.0447745968412735));
#40737=CARTESIAN_POINT('',(-0.00542594286454709,0.0502608408490074,0.0440470889901856));
#40738=CARTESIAN_POINT('',(-0.00419473858185236,0.0501537690094944,0.0421529761750096));
#40739=CARTESIAN_POINT('',(-0.00285634696512304,0.0500785634068521,0.0412068905161621));
#40740=CARTESIAN_POINT('',(-0.000650935336709183,0.0499703363675107,0.0406815858567029));
#40741=CARTESIAN_POINT('',(0.000134804213528367,0.0499317774589967,0.040647075667539));
#40742=CARTESIAN_POINT('',(0.00164167590883445,0.0498578301467811,0.0408733319392693));
#40743=CARTESIAN_POINT('',(0.00235581443537718,0.0498235650214921,0.0411244497890724));
#40744=CARTESIAN_POINT('',(0.00433579048496438,0.0497116180736825,0.0422802806102534));
#40745=CARTESIAN_POINT('',(0.00532798133591556,0.0496404223563881,0.0435544519204082));
#40746=CARTESIAN_POINT('',(0.00596136440889945,0.0495277357420318,0.0457631125755893));
#40747=CARTESIAN_POINT('',(0.00602782510225254,0.0494926654928407,0.0465227163609867));
#40748=CARTESIAN_POINT('',(0.00587578144387195,0.0494200167965288,0.0480299084881039));
#40749=CARTESIAN_POINT('',(0.00564985425987283,0.0493814170334055,0.0487835511151446));
#40750=CARTESIAN_POINT('',(0.00494259057665489,0.0493078302770725,0.0501304404932439));
#40751=CARTESIAN_POINT('',(0.00447054501904416,0.0492734104980149,0.0507235904043108));
#40752=CARTESIAN_POINT('',(0.00330820369998183,0.0491985733649588,0.0517182568428551));
#40753=CARTESIAN_POINT('',(0.00262492815279643,0.0491603448918666,0.0521031329958861));
#40754=CARTESIAN_POINT('',(0.00120628154563118,0.0490901906923114,0.0525826751353633));
#40755=CARTESIAN_POINT('',(0.000433509776971783,0.0490525236996602,0.0526910975554302));
#40756=CARTESIAN_POINT('',(-0.00109522981267062,0.0489775032555947,0.0526064146222846));
#40757=CARTESIAN_POINT('',(-0.00183230736936312,0.0489427841828503,0.052420740389839));
#40758=CARTESIAN_POINT('',(-0.00320894594061515,0.0488696801695706,0.0517811134978896));
#40759=CARTESIAN_POINT('',(-0.00384643009871131,0.0488310652179814,0.0513198122705482));
#40760=CARTESIAN_POINT('',(-0.0048846195327673,0.0487578829350035,0.0502116366112216));
#40761=CARTESIAN_POINT('',(-0.00529110431748674,0.0487232181360992,0.0495697919341571));
#40762=CARTESIAN_POINT('',(-0.00612839681505211,0.0486107234250468,0.0474314972485811));
#40763=CARTESIAN_POINT('',(-0.00611457685600949,0.0485396087928887,0.0458171355611411));
#40764=CARTESIAN_POINT('',(-0.00524213722913385,0.048427304388555,0.0436943384425134));
#40765=CARTESIAN_POINT('',(-0.00482603837135703,0.0483928467330594,0.0430603764341383));
#40766=CARTESIAN_POINT('',(-0.00376799594300458,0.0483193303399575,0.0419679429765193));
#40767=CARTESIAN_POINT('',(-0.00312274344804228,0.0482807259004964,0.0415176983874283));
#40768=CARTESIAN_POINT('',(-0.00173801800845273,0.0482079911864261,0.040902005168776));
#40769=CARTESIAN_POINT('',(-0.000996149780969905,0.0481729914985343,0.0407279060321564));
#40770=CARTESIAN_POINT('',(0.000534394153117021,0.0480978825091583,0.0406687901053457));
#40771=CARTESIAN_POINT('',(0.00130116707099782,0.0480608239545026,0.0407890711511285));
#40772=CARTESIAN_POINT('',(0.00271519543873335,0.0479901493924298,0.04129300994584));
#40773=CARTESIAN_POINT('',(0.00339241327145998,0.04795181491776,0.0416898987444526));
#40774=CARTESIAN_POINT('',(0.00453713172897902,0.0478771427171888,0.0427031030072484));
#40775=CARTESIAN_POINT('',(0.00499890489099844,0.0478428561897471,0.0433031369857737));
#40776=CARTESIAN_POINT('',(0.00568458829322409,0.0477689711909121,0.0446634284610569));
#40777=CARTESIAN_POINT('',(0.00589748451337995,0.0477304029403275,0.0454206299072185));
#40778=CARTESIAN_POINT('',(0.00602435095420808,0.0476581579877139,0.0469273518671414));
#40779=CARTESIAN_POINT('',(0.00594530062534477,0.0476227342193121,0.0476881820089443));
#40780=CARTESIAN_POINT('',(0.00527488903437779,0.0475099725532324,0.0498864194514419));
#40781=CARTESIAN_POINT('',(0.00426061021221676,0.0474386647121791,0.0511439601596007));
#40782=CARTESIAN_POINT('',(0.00226342439943811,0.0473270217408386,0.0522655653621272));
#40783=CARTESIAN_POINT('',(0.00154567488468326,0.0472928157047063,0.0525048960399918));
#40784=CARTESIAN_POINT('',(3.34690311347955E-5,0.0472186066272281,0.0527062554034359));
#40785=CARTESIAN_POINT('',(-0.000751201884539185,0.0471801001602418,0.0526582886400806));
#40786=CARTESIAN_POINT('',(-0.00294324433531448,0.0470725291918558,0.0520977989577606));
#40787=CARTESIAN_POINT('',(-0.00426698861795472,0.0469973641792965,0.0511318035742654));
#40788=CARTESIAN_POINT('',(-0.00546935161541402,0.0468896070560058,0.0492136365489639));
#40789=CARTESIAN_POINT('',(-0.00575400166720846,0.0468510843236482,0.0484807246240088));
#40790=CARTESIAN_POINT('',(-0.00602276831052684,0.0467769448752113,0.0469795167638521));
#40791=CARTESIAN_POINT('',(-0.00601352874026243,0.046742728530006,0.0462229028297622));
#40792=CARTESIAN_POINT('',(-0.00555346454973278,0.0466309965852467,0.0439783825107965));
#40793=CARTESIAN_POINT('',(-0.00466460616883524,0.0465597244451005,0.0426295328261682));
#40794=CARTESIAN_POINT('',(-0.00277511890321976,0.0464469788614523,0.0413214673628862));
#40795=CARTESIAN_POINT('',(-0.00207521442244891,0.0464116591512757,0.0410146196892824));
#40796=CARTESIAN_POINT('',(-0.000600692686594825,0.0463392993614478,0.0406762519575071));
#40797=CARTESIAN_POINT('',(0.000185450487053797,0.0463007206457621,0.0406484824662403));
#40798=CARTESIAN_POINT('',(0.00168942626526117,0.0462269154460345,0.0408871182772802));
#40799=CARTESIAN_POINT('',(0.00240183301928324,0.0461925980123381,0.0411441618553943));
#40800=CARTESIAN_POINT('',(0.00371586134380875,0.0461178769322841,0.0419260256571976));
#40801=CARTESIAN_POINT('',(0.00429996898030531,0.046079570200294,0.0424501078491));
#40802=CARTESIAN_POINT('',(0.00521018041629069,0.0460090375221609,0.0436425722548912));
#40803=CARTESIAN_POINT('',(0.00555890724136474,0.0459718157847407,0.0443372252724397));
#40804=CARTESIAN_POINT('',(0.00596876005678161,0.0458967282161687,0.0458129061804159));
#40805=CARTESIAN_POINT('',(0.00602895839985307,0.0458618124071143,0.0465719721046274));
#40806=CARTESIAN_POINT('',(0.00586429821692855,0.0457889723510128,0.0480791650102269));
#40807=CARTESIAN_POINT('',(0.00563188957955514,0.0457503632704311,0.048830901324237));
#40808=CARTESIAN_POINT('',(0.00491397942628084,0.0456769366830941,0.0501708996225944));
#40809=CARTESIAN_POINT('',(0.0044367389074107,0.0456424275869659,0.0507606627917028));
#40810=CARTESIAN_POINT('',(0.0026802632123916,0.0455300656698666,0.052238501827766));
#40811=CARTESIAN_POINT('',(0.00114679585513747,0.0454589556416382,0.0527432212211965));
#40812=CARTESIAN_POINT('',(-0.00114460042476067,0.0453465090433995,0.0525970595245437));
#40813=CARTESIAN_POINT('',(-0.00187936400588002,0.0453119077743956,0.052405598071758));
#40814=CARTESIAN_POINT('',(-0.00290863757287697,0.0452569493359673,0.0519169443403826));
#40815=CARTESIAN_POINT('',(-0.00323913157385276,0.0452381369348995,0.0517196323634921));
#40816=CARTESIAN_POINT('',(-0.00385599157597277,0.0452005416266125,0.0512652939363906));
#40817=CARTESIAN_POINT('',(-0.00414665186685566,0.0451818020971212,0.0510156819102021));
#40818=CARTESIAN_POINT('',(-0.00444424750172291,0.0451630418632379,0.0507748977756262));
#40819=CARTESIAN_POINT('',(-0.00598201094464286,0.0523196427596204,0.0466759019477942));
#40820=CARTESIAN_POINT('',(-0.00376267327913618,0.0453194007129105,0.0513263583486537));
#40821=CARTESIAN_POINT('',(-0.00376267526235003,0.0452627041593186,0.0513263567440401));
#40822=CARTESIAN_POINT('',(-0.00314499195769477,0.0452627041593186,0.0505629349533058));
#40823=CARTESIAN_POINT('',(-0.00598201094464286,0.0523196427596204,0.0466759019477942));
#40824=CARTESIAN_POINT('',(-0.005,0.058,0.0466759019477942));
#40825=CARTESIAN_POINT('',(-0.00240259137190233,0.0451571425815504,0.0522640639622369));
#40826=CARTESIAN_POINT('',(-0.00310564610108304,0.0529999999,0.0533580384747061));
#40827=CARTESIAN_POINT('',(-0.00310564610108304,0.0529999999,0.0533580384747061));
#40828=CARTESIAN_POINT('',(-0.00310564610108304,0.058,0.0533580384747061));
#40829=CARTESIAN_POINT('',(0.000841253532831189,0.058,0.0472165427652498));
#40830=CARTESIAN_POINT('',(-0.00240259137190233,0.058,0.0522640639622369));
#40831=CARTESIAN_POINT('',(-0.00240259137190233,0.0451571425815504,0.0522640639622369));
#40832=CARTESIAN_POINT('',(-0.00240259137190233,0.0529999999,0.0522640639622369));
#40833=CARTESIAN_POINT('',(-0.00240259137190233,0.0529999999,0.0522640639622369));
#40834=CARTESIAN_POINT('',(-0.00240259137190233,0.0451571425815504,0.0522640639622369));
#40835=CARTESIAN_POINT('',(-0.00240259137190233,0.0529999999,0.0522640639622369));
#40836=CARTESIAN_POINT('',(-0.00408509843756471,0.0529999999,0.0511827823273257));
#40837=CARTESIAN_POINT('',(-0.00240259137190233,0.058,0.0522640639622369));
#40838=CARTESIAN_POINT('',(-0.00408509843756471,0.058,0.0511827823273257));
#40839=CARTESIAN_POINT('',(-0.00408509843756471,0.0451571425815504,0.0511827823273257));
#40840=CARTESIAN_POINT('',(-0.00408509843756471,0.0451571425815504,0.0511827823273257));
#40841=CARTESIAN_POINT('',(-0.00478815316674541,0.0529999999,0.052276756839795));
#40842=CARTESIAN_POINT('',(-0.00478815316674541,0.058,0.052276756839795));
#40843=CARTESIAN_POINT('',(-0.00478815316674541,0.0529999999,0.052276756839795));
#40844=CARTESIAN_POINT('',(-0.00408509843756471,0.0529999999,0.0511827823273257));
#40845=CARTESIAN_POINT('',(-0.00408509843756471,0.058,0.0511827823273257));
#40846=CARTESIAN_POINT('',(-0.00504237695912518,0.0451571425815504,0.0500780240211601));
#40847=CARTESIAN_POINT('',(-0.00622527150851907,0.0529999999,0.0506182338611018));
#40848=CARTESIAN_POINT('',(-0.00622527150851907,0.0529999999,0.0506182338611018));
#40849=CARTESIAN_POINT('',(-0.00622527150851907,0.058,0.0506182338611018));
#40850=CARTESIAN_POINT('',(0.000415415013001893,0.058,0.0475855339431487));
#40851=CARTESIAN_POINT('',(-0.00504237695912518,0.058,0.0500780240211601));
#40852=CARTESIAN_POINT('',(-0.00504237695912518,0.0451571425815504,0.0500780240211601));
#40853=CARTESIAN_POINT('',(-0.00504237695912518,0.0529999999,0.0500780240211601));
#40854=CARTESIAN_POINT('',(-0.00504237695912518,0.0529999999,0.0500780240211601));
#40855=CARTESIAN_POINT('',(-0.00504237695912518,0.0451571425815504,0.0500780240211601));
#40856=CARTESIAN_POINT('',(-0.00504237695912518,0.0529999999,0.0500780240211601));
#40857=CARTESIAN_POINT('',(-0.00587320698512898,0.0529999999,0.0482587600304511));
#40858=CARTESIAN_POINT('',(-0.00504237695912518,0.058,0.0500780240211601));
#40859=CARTESIAN_POINT('',(-0.00587320698512898,0.058,0.0482587600304511));
#40860=CARTESIAN_POINT('',(-0.00587320698512898,0.0451571425815504,0.0482587600304511));
#40861=CARTESIAN_POINT('',(-0.00587320698512898,0.0451571425815504,0.0482587600304511));
#40862=CARTESIAN_POINT('',(-0.00705610153452287,0.0529999999,0.0487989698703928));
#40863=CARTESIAN_POINT('',(-0.00705610153452287,0.058,0.0487989698703928));
#40864=CARTESIAN_POINT('',(-0.00705610153452287,0.0529999999,0.0487989698703928));
#40865=CARTESIAN_POINT('',(-0.00587320698512898,0.0529999999,0.0482587600304511));
#40866=CARTESIAN_POINT('',(-0.00587320698512898,0.058,0.0482587600304511));
#40867=CARTESIAN_POINT('',(-0.00608124348955888,0.0451571425815504,0.0468118343600355));
#40868=CARTESIAN_POINT('',(-0.00736841719766689,0.0529999999,0.0466267667202085));
#40869=CARTESIAN_POINT('',(-0.00736841719766689,0.0529999999,0.0466267667202085));
#40870=CARTESIAN_POINT('',(-0.00736841719766689,0.058,0.0466267667202085));
#40871=CARTESIAN_POINT('',(-0.000142314838273275,0.058,0.0476657233896751));
#40872=CARTESIAN_POINT('',(-0.00608124348955888,0.058,0.0468118343600355));
#40873=CARTESIAN_POINT('',(-0.00608124348955888,0.0451571425815504,0.0468118343600355));
#40874=CARTESIAN_POINT('',(-0.00608124348955888,0.0529999999,0.0468118343600355));
#40875=CARTESIAN_POINT('',(-0.00608124348955888,0.0529999999,0.0468118343600355));
#40876=CARTESIAN_POINT('',(-0.00608124348955888,0.0451571425815504,0.0468118343600355));
#40877=CARTESIAN_POINT('',(-0.00608124348955888,0.0529999999,0.0468118343600355));
#40878=CARTESIAN_POINT('',(-0.00579661381301233,0.0529999999,0.0448321914762736));
#40879=CARTESIAN_POINT('',(-0.00608124348955888,0.058,0.0468118343600355));
#40880=CARTESIAN_POINT('',(-0.00579661381301233,0.058,0.0448321914762736));
#40881=CARTESIAN_POINT('',(-0.00579661381301233,0.0451571425815504,0.0448321914762736));
#40882=CARTESIAN_POINT('',(-0.00579661381301233,0.0451571425815504,0.0448321914762736));
#40883=CARTESIAN_POINT('',(-0.00708378752112034,0.0529999999,0.0446471238364467));
#40884=CARTESIAN_POINT('',(-0.00708378752112034,0.058,0.0446471238364467));
#40885=CARTESIAN_POINT('',(-0.00708378752112034,0.0529999999,0.0446471238364467));
#40886=CARTESIAN_POINT('',(-0.00579661381301233,0.0529999999,0.0448321914762736));
#40887=CARTESIAN_POINT('',(-0.00579661381301233,0.058,0.0448321914762736));
#40888=CARTESIAN_POINT('',(-0.00518935818007087,0.0451571425815504,0.0435024871184768));
#40889=CARTESIAN_POINT('',(-0.00617214248930353,0.0529999999,0.0426508996669008));
#40890=CARTESIAN_POINT('',(-0.00617214248930353,0.0529999999,0.0426508996669008));
#40891=CARTESIAN_POINT('',(-0.00617214248930353,0.058,0.0426508996669008));
#40892=CARTESIAN_POINT('',(-0.00065486073394528,0.058,0.0474316515221485));
#40893=CARTESIAN_POINT('',(-0.00518935818007087,0.058,0.0435024871184768));
#40894=CARTESIAN_POINT('',(-0.00518935818007087,0.0451571425815504,0.0435024871184768));
#40895=CARTESIAN_POINT('',(-0.00518935818007087,0.0529999999,0.0435024871184768));
#40896=CARTESIAN_POINT('',(-0.00518935818007087,0.0529999999,0.0435024871184768));
#40897=CARTESIAN_POINT('',(-0.00518935818007087,0.0451571425815504,0.0435024871184768));
#40898=CARTESIAN_POINT('',(-0.00518935818007087,0.0529999999,0.0435024871184768));
#40899=CARTESIAN_POINT('',(-0.0038796367121803,0.0529999999,0.0419909879697682));
#40900=CARTESIAN_POINT('',(-0.00518935818007087,0.058,0.0435024871184768));
#40901=CARTESIAN_POINT('',(-0.0038796367121803,0.058,0.0419909879697682));
#40902=CARTESIAN_POINT('',(-0.0038796367121803,0.0451571425815504,0.0419909879697682));
#40903=CARTESIAN_POINT('',(-0.0038796367121803,0.0451571425815504,0.0419909879697682));
#40904=CARTESIAN_POINT('',(-0.00486242102141297,0.0529999999,0.0411394005181923));
#40905=CARTESIAN_POINT('',(-0.00486242102141297,0.058,0.0411394005181923));
#40906=CARTESIAN_POINT('',(-0.00486242102141297,0.0529999999,0.0411394005181923));
#40907=CARTESIAN_POINT('',(-0.0038796367121803,0.0529999999,0.0419909879697682));
#40908=CARTESIAN_POINT('',(-0.0038796367121803,0.058,0.0419909879697682));
#40909=CARTESIAN_POINT('',(-0.00264988831466312,0.0451571425815504,0.0412006766629487));
#40910=CARTESIAN_POINT('',(-0.00301625615086116,0.0529999999,0.0399529423984696));
#40911=CARTESIAN_POINT('',(-0.00301625615086116,0.0529999999,0.0399529423984696));
#40912=CARTESIAN_POINT('',(-0.00301625615086115,0.058,0.0399529423984696));
#40913=CARTESIAN_POINT('',(-0.000959492973614494,0.058,0.0469576345046356));
#40914=CARTESIAN_POINT('',(-0.00264988831466312,0.058,0.0412006766629487));
#40915=CARTESIAN_POINT('',(-0.00264988831466312,0.0451571425815504,0.0412006766629487));
#40916=CARTESIAN_POINT('',(-0.00264988831466312,0.0529999999,0.0412006766629487));
#40917=CARTESIAN_POINT('',(-0.00264988831466312,0.0529999999,0.0412006766629487));
#40918=CARTESIAN_POINT('',(-0.00264988831466312,0.0451571425815504,0.0412006766629487));
#40919=CARTESIAN_POINT('',(-0.00264988831466312,0.0529999999,0.0412006766629487));
#40920=CARTESIAN_POINT('',(-0.000730902367434127,0.0529999999,0.0406372115492658));
#40921=CARTESIAN_POINT('',(-0.00264988831466312,0.058,0.0412006766629487));
#40922=CARTESIAN_POINT('',(-0.000730902367434127,0.058,0.0406372115492658));
#40923=CARTESIAN_POINT('',(-0.000730902367434127,0.0451571425815504,0.0406372115492658));
#40924=CARTESIAN_POINT('',(-0.000730902367434127,0.0451571425815504,0.0406372115492658));
#40925=CARTESIAN_POINT('',(-0.00109727020363217,0.0529999999,0.0393894772847867));
#40926=CARTESIAN_POINT('',(-0.00109727020363217,0.058,0.0393894772847867));
#40927=CARTESIAN_POINT('',(-0.00109727020363217,0.0529999999,0.0393894772847867));
#40928=CARTESIAN_POINT('',(-0.000730902367434127,0.0529999999,0.0406372115492658));
#40929=CARTESIAN_POINT('',(-0.000730902367434127,0.058,0.0406372115492658));
#40930=CARTESIAN_POINT('',(0.00073090236743404,0.0451571425815504,0.0406372115492658));
#40931=CARTESIAN_POINT('',(0.00109727020363206,0.0529999999,0.0393894772847867));
#40932=CARTESIAN_POINT('',(0.00109727020363206,0.0529999999,0.0393894772847867));
#40933=CARTESIAN_POINT('',(0.00109727020363206,0.058,0.0393894772847867));
#40934=CARTESIAN_POINT('',(-0.000959492973614499,0.058,0.0463941693909528));
#40935=CARTESIAN_POINT('',(0.00073090236743404,0.058,0.0406372115492658));
#40936=CARTESIAN_POINT('',(0.00073090236743404,0.0451571425815504,0.0406372115492658));
#40937=CARTESIAN_POINT('',(0.00073090236743404,0.0529999999,0.0406372115492658));
#40938=CARTESIAN_POINT('',(0.00073090236743404,0.0529999999,0.0406372115492658));
#40939=CARTESIAN_POINT('',(0.00073090236743404,0.0451571425815504,0.0406372115492658));
#40940=CARTESIAN_POINT('',(0.00073090236743404,0.0529999999,0.0406372115492658));
#40941=CARTESIAN_POINT('',(0.00264988831466304,0.0529999999,0.0412006766629486));
#40942=CARTESIAN_POINT('',(0.00073090236743404,0.058,0.0406372115492658));
#40943=CARTESIAN_POINT('',(0.00264988831466304,0.058,0.0412006766629486));
#40944=CARTESIAN_POINT('',(0.00264988831466304,0.0451571425815504,0.0412006766629486));
#40945=CARTESIAN_POINT('',(0.00264988831466304,0.0451571425815504,0.0412006766629486));
#40946=CARTESIAN_POINT('',(0.00301625615086107,0.0529999999,0.0399529423984695));
#40947=CARTESIAN_POINT('',(0.00301625615086107,0.058,0.0399529423984695));
#40948=CARTESIAN_POINT('',(0.00301625615086107,0.0529999999,0.0399529423984695));
#40949=CARTESIAN_POINT('',(0.00264988831466304,0.0529999999,0.0412006766629486));
#40950=CARTESIAN_POINT('',(0.00264988831466304,0.058,0.0412006766629486));
#40951=CARTESIAN_POINT('',(0.00387963671218024,0.0451571425815504,0.0419909879697682));
#40952=CARTESIAN_POINT('',(0.00486242102141288,0.0529999999,0.0411394005181922));
#40953=CARTESIAN_POINT('',(0.00486242102141288,0.0529999999,0.0411394005181922));
#40954=CARTESIAN_POINT('',(0.00486242102141289,0.058,0.0411394005181921));
#40955=CARTESIAN_POINT('',(-0.000654860733945287,0.058,0.0459201523734399));
#40956=CARTESIAN_POINT('',(0.00387963671218024,0.058,0.0419909879697682));
#40957=CARTESIAN_POINT('',(0.00387963671218024,0.0451571425815504,0.0419909879697682));
#40958=CARTESIAN_POINT('',(0.00387963671218024,0.0529999999,0.0419909879697682));
#40959=CARTESIAN_POINT('',(0.00387963671218024,0.0529999999,0.0419909879697682));
#40960=CARTESIAN_POINT('',(0.00387963671218024,0.0451571425815504,0.0419909879697682));
#40961=CARTESIAN_POINT('',(0.00387963671218024,0.0529999999,0.0419909879697682));
#40962=CARTESIAN_POINT('',(0.00518935818007081,0.0529999999,0.0435024871184767));
#40963=CARTESIAN_POINT('',(0.00387963671218024,0.058,0.0419909879697682));
#40964=CARTESIAN_POINT('',(0.00518935818007081,0.058,0.0435024871184767));
#40965=CARTESIAN_POINT('',(0.00518935818007081,0.0451571425815504,0.0435024871184767));
#40966=CARTESIAN_POINT('',(0.00518935818007081,0.0451571425815504,0.0435024871184767));
#40967=CARTESIAN_POINT('',(0.00617214248930346,0.0529999999,0.0426508996669007));
#40968=CARTESIAN_POINT('',(0.00617214248930346,0.058,0.0426508996669007));
#40969=CARTESIAN_POINT('',(0.00617214248930346,0.0529999999,0.0426508996669007));
#40970=CARTESIAN_POINT('',(0.00518935818007081,0.0529999999,0.0435024871184767));
#40971=CARTESIAN_POINT('',(0.00518935818007081,0.058,0.0435024871184767));
#40972=CARTESIAN_POINT('',(0.0057966138130123,0.0451571425815504,0.0448321914762735));
#40973=CARTESIAN_POINT('',(0.00708378752112031,0.0529999999,0.0446471238364465));
#40974=CARTESIAN_POINT('',(0.00708378752112031,0.0529999999,0.0446471238364465));
#40975=CARTESIAN_POINT('',(0.00708378752112031,0.058,0.0446471238364465));
#40976=CARTESIAN_POINT('',(-0.000142314838273289,0.058,0.0456860805059133));
#40977=CARTESIAN_POINT('',(0.0057966138130123,0.058,0.0448321914762735));
#40978=CARTESIAN_POINT('',(0.0057966138130123,0.0451571425815504,0.0448321914762735));
#40979=CARTESIAN_POINT('',(0.0057966138130123,0.0529999999,0.0448321914762735));
#40980=CARTESIAN_POINT('',(0.0057966138130123,0.0529999999,0.0448321914762735));
#40981=CARTESIAN_POINT('',(0.0057966138130123,0.0451571425815504,0.0448321914762735));
#40982=CARTESIAN_POINT('',(0.0057966138130123,0.0529999999,0.0448321914762735));
#40983=CARTESIAN_POINT('',(0.00608124348955888,0.0529999999,0.0468118343600354));
#40984=CARTESIAN_POINT('',(0.0057966138130123,0.058,0.0448321914762735));
#40985=CARTESIAN_POINT('',(0.00608124348955888,0.058,0.0468118343600354));
#40986=CARTESIAN_POINT('',(0.00608124348955888,0.0451571425815504,0.0468118343600354));
#40987=CARTESIAN_POINT('',(0.00608124348955888,0.0451571425815504,0.0468118343600354));
#40988=CARTESIAN_POINT('',(0.00736841719766689,0.0529999999,0.0466267667202084));
#40989=CARTESIAN_POINT('',(0.00736841719766689,0.058,0.0466267667202084));
#40990=CARTESIAN_POINT('',(0.00736841719766689,0.0529999999,0.0466267667202084));
#40991=CARTESIAN_POINT('',(0.00608124348955888,0.0529999999,0.0468118343600354));
#40992=CARTESIAN_POINT('',(0.00608124348955888,0.058,0.0468118343600354));
#40993=CARTESIAN_POINT('',(0.005873206985129,0.0451571425815504,0.048258760030451));
#40994=CARTESIAN_POINT('',(0.0070561015345229,0.0529999999,0.0487989698703927));
#40995=CARTESIAN_POINT('',(0.0070561015345229,0.0529999999,0.0487989698703927));
#40996=CARTESIAN_POINT('',(0.0070561015345229,0.058,0.0487989698703927));
#40997=CARTESIAN_POINT('',(0.000415415013001886,0.058,0.0457662699524397));
#40998=CARTESIAN_POINT('',(0.005873206985129,0.058,0.048258760030451));
#40999=CARTESIAN_POINT('',(0.005873206985129,0.0451571425815504,0.048258760030451));
#41000=CARTESIAN_POINT('',(0.005873206985129,0.0529999999,0.048258760030451));
#41001=CARTESIAN_POINT('',(0.005873206985129,0.0529999999,0.048258760030451));
#41002=CARTESIAN_POINT('',(0.005873206985129,0.0451571425815504,0.048258760030451));
#41003=CARTESIAN_POINT('',(0.005873206985129,0.0529999999,0.048258760030451));
#41004=CARTESIAN_POINT('',(0.00504237695912523,0.0529999999,0.05007802402116));
#41005=CARTESIAN_POINT('',(0.005873206985129,0.058,0.048258760030451));
#41006=CARTESIAN_POINT('',(0.00504237695912523,0.058,0.05007802402116));
#41007=CARTESIAN_POINT('',(0.00504237695912523,0.0451571425815504,0.05007802402116));
#41008=CARTESIAN_POINT('',(0.00504237695912523,0.0451571425815504,0.05007802402116));
#41009=CARTESIAN_POINT('',(0.00622527150851913,0.0529999999,0.0506182338611017));
#41010=CARTESIAN_POINT('',(0.00622527150851913,0.058,0.0506182338611017));
#41011=CARTESIAN_POINT('',(0.00622527150851913,0.0529999999,0.0506182338611017));
#41012=CARTESIAN_POINT('',(0.00504237695912523,0.0529999999,0.05007802402116));
#41013=CARTESIAN_POINT('',(0.00504237695912523,0.058,0.05007802402116));
#41014=CARTESIAN_POINT('',(0.00408509843756477,0.0451571425815504,0.0511827823273257));
#41015=CARTESIAN_POINT('',(0.00478815316674549,0.0529999999,0.0522767568397949));
#41016=CARTESIAN_POINT('',(0.00478815316674549,0.0529999999,0.0522767568397949));
#41017=CARTESIAN_POINT('',(0.00478815316674549,0.058,0.0522767568397949));
#41018=CARTESIAN_POINT('',(0.000841253532831179,0.058,0.0461352611303386));
#41019=CARTESIAN_POINT('',(0.00408509843756477,0.058,0.0511827823273257));
#41020=CARTESIAN_POINT('',(0.00408509843756477,0.0451571425815504,0.0511827823273257));
#41021=CARTESIAN_POINT('',(0.00408509843756477,0.0529999999,0.0511827823273257));
#41022=CARTESIAN_POINT('',(0.00408509843756477,0.0529999999,0.0511827823273257));
#41023=CARTESIAN_POINT('',(0.00408509843756477,0.0451571425815504,0.0511827823273257));
#41024=CARTESIAN_POINT('',(0.00408509843756477,0.0529999999,0.0511827823273257));
#41025=CARTESIAN_POINT('',(0.00240259137190241,0.0529999999,0.0522640639622369));
#41026=CARTESIAN_POINT('',(0.00408509843756477,0.058,0.0511827823273257));
#41027=CARTESIAN_POINT('',(0.00240259137190241,0.058,0.0522640639622369));
#41028=CARTESIAN_POINT('',(0.00240259137190241,0.0451571425815504,0.0522640639622369));
#41029=CARTESIAN_POINT('',(0.00240259137190241,0.0451571425815504,0.0522640639622369));
#41030=CARTESIAN_POINT('',(0.00310564610108313,0.0529999999,0.0533580384747061));
#41031=CARTESIAN_POINT('',(0.00310564610108313,0.058,0.0533580384747061));
#41032=CARTESIAN_POINT('',(0.00310564610108313,0.0529999999,0.0533580384747061));
#41033=CARTESIAN_POINT('',(0.00240259137190241,0.0529999999,0.0522640639622369));
#41034=CARTESIAN_POINT('',(0.00240259137190241,0.058,0.0522640639622369));
#41035=CARTESIAN_POINT('',(0.001,0.0451571425815504,0.0526759019477942));
#41036=CARTESIAN_POINT('',(0.001,0.0529999999,0.0539763119547365));
#41037=CARTESIAN_POINT('',(0.001,0.0529999999,0.0539763119547365));
#41038=CARTESIAN_POINT('',(0.001,0.058,0.0539763119547365));
#41039=CARTESIAN_POINT('',(0.001,0.058,0.0466759019477942));
#41040=CARTESIAN_POINT('',(0.001,0.058,0.0526759019477942));
#41041=CARTESIAN_POINT('',(0.001,0.0451571425815504,0.0526759019477942));
#41042=CARTESIAN_POINT('',(0.001,0.0529999999,0.0526759019477942));
#41043=CARTESIAN_POINT('',(0.001,0.0529999999,0.0526759019477942));
#41044=CARTESIAN_POINT('',(0.001,0.0451571425815504,0.0526759019477942));
#41045=CARTESIAN_POINT('',(0.001,0.0529999999,0.0526759019477942));
#41046=CARTESIAN_POINT('',(-0.001,0.0529999999,0.0526759019477942));
#41047=CARTESIAN_POINT('',(0.001,0.058,0.0526759019477942));
#41048=CARTESIAN_POINT('',(-0.001,0.058,0.0526759019477942));
#41049=CARTESIAN_POINT('',(-0.001,0.0451571425815504,0.0526759019477942));
#41050=CARTESIAN_POINT('',(-0.001,0.0451571425815504,0.0526759019477942));
#41051=CARTESIAN_POINT('',(-0.001,0.0529999999,0.0539763119547365));
#41052=CARTESIAN_POINT('',(-0.001,0.058,0.0539763119547365));
#41053=CARTESIAN_POINT('',(-0.001,0.0529999999,0.0539763119547365));
#41054=CARTESIAN_POINT('',(-0.001,0.0529999999,0.0526759019477942));
#41055=CARTESIAN_POINT('',(-0.001,0.058,0.0526759019477942));
#41056=CARTESIAN_POINT('',(0.,0.058,0.0466759019477942));
#41057=CARTESIAN_POINT('',(0.,0.058,0.0466759019477942));
#41058=CARTESIAN_POINT('',(0.,0.058,0.0466759019477942));
#41059=CARTESIAN_POINT('',(0.,0.058,0.0466759019477942));
#41060=CARTESIAN_POINT('',(0.,0.058,0.0466759019477942));
#41061=CARTESIAN_POINT('',(0.,0.058,0.0466759019477942));
#41062=CARTESIAN_POINT('',(0.,0.058,0.0466759019477942));
#41063=CARTESIAN_POINT('',(0.,0.058,0.0466759019477942));
#41064=CARTESIAN_POINT('',(0.,0.058,0.0466759019477942));
#41065=CARTESIAN_POINT('',(0.,0.058,0.0466759019477942));
#41066=CARTESIAN_POINT('',(0.,0.058,0.0466759019477942));
#41067=CARTESIAN_POINT('',(0.,0.058,0.0466759019477942));
#41068=CARTESIAN_POINT('',(0.,0.058,0.0466759019477942));
#41069=CARTESIAN_POINT('',(0.,0.058,0.0470759019477942));
#41070=CARTESIAN_POINT('',(0.,0.0529999999,0.0466759019477942));
#41071=CARTESIAN_POINT('',(0.,0.0529999999,0.0466759019477942));
#41072=CARTESIAN_POINT('',(0.,0.0529999999,0.0466759019477942));
#41073=CARTESIAN_POINT('',(0.,0.0529999999,0.0466759019477942));
#41074=CARTESIAN_POINT('',(0.,0.0529999999,0.0466759019477942));
#41075=CARTESIAN_POINT('',(0.,0.0529999999,0.0466759019477942));
#41076=CARTESIAN_POINT('',(0.,0.0529999999,0.0466759019477942));
#41077=CARTESIAN_POINT('',(0.,0.0529999999,0.0466759019477942));
#41078=CARTESIAN_POINT('',(0.,0.0529999999,0.0466759019477942));
#41079=CARTESIAN_POINT('',(0.,0.0529999999,0.0466759019477942));
#41080=CARTESIAN_POINT('',(0.,0.0529999999,0.0466759019477942));
#41081=CARTESIAN_POINT('',(0.,0.0529999999,0.0466759019477942));
#41082=CARTESIAN_POINT('',(0.,0.0529999999,0.0466759019477942));
#41083=CARTESIAN_POINT('',(0.,0.0529999999,0.0466759019477942));
#41084=CARTESIAN_POINT('',(0.,0.043,0.0466759019477942));
#41085=CARTESIAN_POINT('',(0.,0.043,0.0466759019477942));
#41086=CARTESIAN_POINT('',(0.,0.043,0.0516759019477942));
#41087=CARTESIAN_POINT('',(0.,0.043,0.0466759019477942));
#41088=CARTESIAN_POINT('',(0.,0.043,0.0470759019477942));
#41089=CARTESIAN_POINT('',(0.,0.0529999999,0.0466759019477942));
#41090=CARTESIAN_POINT('',(0.,0.0529999999,0.0466759019477942));
#41091=CARTESIAN_POINT('',(0.,0.0529999999,0.0466759019477942));
#41092=CARTESIAN_POINT('',(0.,0.0529999999,0.0466759019477942));
#41093=CARTESIAN_POINT('',(0.,0.0529999999,0.0466759019477942));
#41094=CARTESIAN_POINT('',(0.,0.0529999999,0.0466759019477942));
#41095=CARTESIAN_POINT('',(0.,0.0529999999,0.0466759019477942));
#41096=CARTESIAN_POINT('',(0.,0.0529999999,0.0466759019477942));
#41097=CARTESIAN_POINT('',(0.,0.0529999999,0.0466759019477942));
#41098=CARTESIAN_POINT('',(0.,0.0529999999,0.0466759019477942));
#41099=CARTESIAN_POINT('',(0.,0.058,0.0466759019477942));
#41100=CARTESIAN_POINT('',(0.,-0.053,0.0466759019477942));
#45463=MECHANICAL_DESIGN_GEOMETRIC_PRESENTATION_REPRESENTATION('',(#13551),#45464);
#45464=(
GEOMETRIC_REPRESENTATION_CONTEXT(3)
GLOBAL_UNCERTAINTY_ASSIGNED_CONTEXT((#45492))
GLOBAL_UNIT_ASSIGNED_CONTEXT((#45522,#45521,#45520))
REPRESENTATION_CONTEXT('MAS-690','TOP_LEVEL_ASSEMBLY_PART')
);
#45487=(
GEOMETRIC_REPRESENTATION_CONTEXT(3)
GLOBAL_UNCERTAINTY_ASSIGNED_CONTEXT((#45515))
GLOBAL_UNIT_ASSIGNED_CONTEXT((#45522,#45521,#45520))
REPRESENTATION_CONTEXT('refill_screw','COMPONENT_PART')
);
#45492=UNCERTAINTY_MEASURE_WITH_UNIT(LENGTH_MEASURE(1.E-8),#45522,
'DISTANCE_ACCURACY_VALUE','Maximum Tolerance applied to model');
#45515=UNCERTAINTY_MEASURE_WITH_UNIT(LENGTH_MEASURE(2.E-5),#45522,
'DISTANCE_ACCURACY_VALUE','Maximum Tolerance applied to model');
#45520=(
NAMED_UNIT(*)
SI_UNIT($,.STERADIAN.)
SOLID_ANGLE_UNIT()
);
#45521=(
NAMED_UNIT(*)
PLANE_ANGLE_UNIT()
SI_UNIT($,.RADIAN.)
);
#45522=(
LENGTH_UNIT()
NAMED_UNIT(*)
SI_UNIT($,.METRE.)
);
#45574=PRODUCT_DEFINITION_SHAPE('','',#45608);
#45608=PRODUCT_DEFINITION('','',#45664,#45636);
#45636=PRODUCT_DEFINITION_CONTEXT('',#45782,'design');
#45664=PRODUCT_DEFINITION_FORMATION_WITH_SPECIFIED_SOURCE('','',#45720,
 .NOT_KNOWN.);
#45720=PRODUCT('refill_screw','refill_screw','refill_screw',(#45776));
#45776=PRODUCT_CONTEXT('',#45782,'mechanical');
#45782=APPLICATION_CONTEXT('managed model based 3d engineering');
ENDSEC;
END-ISO-10303-21;
